ISO-10303-21;
HEADER;
FILE_DESCRIPTION (('STEP AP214'),
    '1' );
FILE_NAME ('rack_ISO - Rack-spur - rectangular 1M 20PA 12FW 5PH 25L---SAll.step',
    '2026-10-03T18:28:46',
    ( '' ),
    ( '' ),
    'SwSTEP 2.0',
    'SolidWorks 2026',
    '' );
FILE_SCHEMA (( 'AUTOMOTIVE_DESIGN' ));
ENDSEC;

DATA;
#2=ORIENTED_EDGE ( 'NONE', *, *, #1158, .F. ) ;
#5=DIRECTION ( 'NONE',  ( 0.3420201433256627732, 0.9396926207859105373, 0.000000000000000000 ) ) ;
#19=ADVANCED_FACE ( 'NONE', ( #1564 ), #26, .F. ) ;
#21=EDGE_CURVE ( 'NONE', #307, #4726, #872, .T. ) ;
#26=PLANE ( 'NONE',  #10330 ) ;
#31=VECTOR ( 'NONE', #1258, 1000.000000000000000 ) ;
#33=EDGE_LOOP ( 'NONE', ( #1862, #211, #6876, #1898 ) ) ;
#36=EDGE_CURVE ( 'NONE', #3582, #9702, #3146, .T. ) ;
#37=DIRECTION ( 'NONE',  ( 0.000000000000000000, 0.000000000000000000, 1.000000000000000000 ) ) ;
#41=FACE_OUTER_BOUND ( 'NONE', #7858, .T. ) ;
#44=ORIENTED_EDGE ( 'NONE', *, *, #5320, .F. ) ;
#46=FACE_OUTER_BOUND ( 'NONE', #10061, .T. ) ;
#55=ORIENTED_EDGE ( 'NONE', *, *, #4599, .F. ) ;
#57=FACE_OUTER_BOUND ( 'NONE', #643, .T. ) ;
#59=DIRECTION ( 'NONE',  ( 0.9396926207859105373, -0.3420201433256627732, 0.000000000000000000 ) ) ;
#62=CARTESIAN_POINT ( 'NONE',  ( 15.26352788033274699, -7.750000000000000000, -12.00000000000000000 ) ) ;
#63=EDGE_CURVE ( 'NONE', #2398, #931, #4099, .T. ) ;
#72=CARTESIAN_POINT ( 'NONE',  ( 8.161409553233806236, 6.000000000000000000, 0.000000000000000000 ) ) ;
#74=CARTESIAN_POINT ( 'NONE',  ( 4.414205890716556446, -10.02539999999999942, 0.000000000000000000 ) ) ;
#78=CARTESIAN_POINT ( 'NONE',  ( 11.30300220323380600, -10.00000000000000000, -12.00000000000000000 ) ) ;
#81=EDGE_CURVE ( 'NONE', #3937, #2835, #7332, .T. ) ;
#83=EDGE_CURVE ( 'NONE', #8159, #4280, #2511, .T. ) ;
#86=ORIENTED_EDGE ( 'NONE', *, *, #8247, .T. ) ;
#87=CARTESIAN_POINT ( 'NONE',  ( 16.97133164676619899, -10.00000000000000000, -12.00000000000000000 ) ) ;
#89=ORIENTED_EDGE ( 'NONE', *, *, #4537, .T. ) ;
#95=ORIENTED_EDGE ( 'NONE', *, *, #4515, .F. ) ;
#97=VECTOR ( 'NONE', #1529, 1000.000000000000000 ) ;
#99=DIRECTION ( 'NONE',  ( -0.000000000000000000, -1.000000000000000000, -0.000000000000000000 ) ) ;
#100=FILL_AREA_STYLE_COLOUR ( '', #7967 ) ;
#108=AXIS2_PLACEMENT_3D ( 'NONE', #9729, #5879, #8289 ) ;
#109=ORIENTED_EDGE ( 'NONE', *, *, #1183, .T. ) ;
#114=CARTESIAN_POINT ( 'NONE',  ( 25.57717656966725883, -7.750000000000000000, -12.00000000000000000 ) ) ;
#115=VECTOR ( 'NONE', #2977, 1000.000000000000000 ) ;
#119=DIRECTION ( 'NONE',  ( 0.000000000000000000, 0.000000000000000000, 1.000000000000000000 ) ) ;
#124=CARTESIAN_POINT ( 'NONE',  ( 0.000000000000000000, 0.000000000000000000, -12.00000000000000000 ) ) ;
#126=PLANE ( 'NONE',  #1722 ) ;
#138=VERTEX_POINT ( 'NONE', #1768 ) ;
#140=LINE ( 'NONE', #6544, #6932 ) ;
#146=CARTESIAN_POINT ( 'NONE',  ( 12.12193523033274545, 3.750000000000000000, 0.000000000000000000 ) ) ;
#147=ORIENTED_EDGE ( 'NONE', *, *, #2859, .T. ) ;
#150=EDGE_CURVE ( 'NONE', #6457, #8930, #2463, .T. ) ;
#154=DIRECTION ( 'NONE',  ( 1.000000000000000000, 0.000000000000000000, 0.000000000000000000 ) ) ;
#155=AXIS2_PLACEMENT_3D ( 'NONE', #4132, #7961, #9612 ) ;
#156=ORIENTED_EDGE ( 'NONE', *, *, #9552, .F. ) ;
#160=ORIENTED_EDGE ( 'NONE', *, *, #6778, .T. ) ;
#167=LINE ( 'NONE', #2277, #6439 ) ;
#170=CARTESIAN_POINT ( 'NONE',  ( 5.019816903233806471, 6.000000000000000000, -12.00000000000000000 ) ) ;
#171=VECTOR ( 'NONE', #6634, 1000.000000000000000 ) ;
#173=VECTOR ( 'NONE', #7941, 1000.000000000000000 ) ;
#181=VECTOR ( 'NONE', #6809, 1000.000000000000000 ) ;
#186=ORIENTED_EDGE ( 'NONE', *, *, #3227, .F. ) ;
#192=ORIENTED_EDGE ( 'NONE', *, *, #4599, .T. ) ;
#197=ORIENTED_EDGE ( 'NONE', *, *, #1437, .F. ) ;
#203=EDGE_CURVE ( 'NONE', #3477, #3593, #1173, .T. ) ;
#204=ORIENTED_EDGE ( 'NONE', *, *, #9490, .F. ) ;
#211=ORIENTED_EDGE ( 'NONE', *, *, #1815, .F. ) ;
#224=ORIENTED_EDGE ( 'NONE', *, *, #10008, .F. ) ;
#230=VECTOR ( 'NONE', #6076, 1000.000000000000000 ) ;
#231=PLANE ( 'NONE',  #1121 ) ;
#242=DIRECTION ( 'NONE',  ( 0.9396926207859105373, 0.3420201433256627732, 0.000000000000000000 ) ) ;
#243=CARTESIAN_POINT ( 'NONE',  ( 5.010572059283444624, 6.025400000000000311, -12.00000000000000000 ) ) ;
#244=VERTEX_POINT ( 'NONE', #6788 ) ;
#247=VERTEX_POINT ( 'NONE', #6726 ) ;
#255=( NAMED_UNIT ( * ) SI_UNIT ( $, .STERADIAN. ) SOLID_ANGLE_UNIT ( ) );
#256=ORIENTED_EDGE ( 'NONE', *, *, #1778, .T. ) ;
#262=EDGE_LOOP ( 'NONE', ( #2145, #5885, #3192, #5080 ) ) ;
#265=VECTOR ( 'NONE', #8626, 1000.000000000000000 ) ;
#266=ORIENTED_EDGE ( 'NONE', *, *, #5238, .F. ) ;
#267=CARTESIAN_POINT ( 'NONE',  ( 25.00000000000000000, -4.000000000000000000, -12.00000000000000000 ) ) ;
#270=CARTESIAN_POINT ( 'NONE',  ( 0.000000000000000000, 6.000000000000000000, 0.000000000000000000 ) ) ;
#271=VECTOR ( 'NONE', #4642, 1000.000000000000000 ) ;
#277=ADVANCED_FACE ( 'NONE', ( #8443 ), #9887, .T. ) ;
#283=FACE_OUTER_BOUND ( 'NONE', #3268, .T. ) ;
#287=EDGE_CURVE ( 'NONE', #717, #2796, #5043, .T. ) ;
#295=PLANE ( 'NONE',  #8652 ) ;
#297=EDGE_CURVE ( 'NONE', #931, #7411, #3459, .T. ) ;
#307=VERTEX_POINT ( 'NONE', #8395 ) ;
#311=EDGE_LOOP ( 'NONE', ( #449, #2452, #4667, #4816 ) ) ;
#315=CARTESIAN_POINT ( 'NONE',  ( 19.29399126966725575, -7.750000000000000000, -12.00000000000000000 ) ) ;
#316=PLANE ( 'NONE',  #9995 ) ;
#323=PLANE ( 'NONE',  #6266 ) ;
#329=FACE_OUTER_BOUND ( 'NONE', #5922, .T. ) ;
#333=AXIS2_PLACEMENT_3D ( 'NONE', #1807, #5615, #7419 ) ;
#345=LINE ( 'NONE', #6849, #7114 ) ;
#355=EDGE_LOOP ( 'NONE', ( #1789, #5959, #4901, #4754 ) ) ;
#364=ORIENTED_EDGE ( 'NONE', *, *, #1850, .F. ) ;
#365=AXIS2_PLACEMENT_3D ( 'NONE', #4043, #10034, #4146 ) ;
#369=CARTESIAN_POINT ( 'NONE',  ( 6.727620669667255804, -7.750000000000000000, 0.000000000000000000 ) ) ;
#372=CARTESIAN_POINT ( 'NONE',  ( 18.40512053033274853, 3.750000000000000000, -12.00000000000000000 ) ) ;
#377=DIRECTION ( 'NONE',  ( 0.9396926207859105373, -0.3420201433256627732, 0.000000000000000000 ) ) ;
#379=CARTESIAN_POINT ( 'NONE',  ( 9.869213319667256457, -7.750000000000000000, -12.00000000000000000 ) ) ;
#387=EDGE_CURVE ( 'NONE', #1597, #8333, #6145, .T. ) ;
#390=ORIENTED_EDGE ( 'NONE', *, *, #4857, .T. ) ;
#391=VECTOR ( 'NONE', #4021, 1000.000000000000000 ) ;
#394=CARTESIAN_POINT ( 'NONE',  ( 25.00000000000000000, 0.000000000000000000, -12.00000000000000000 ) ) ;
#399=ADVANCED_FACE ( 'NONE', ( #3026 ), #9451, .T. ) ;
#406=DIRECTION ( 'NONE',  ( 1.000000000000000000, 0.000000000000000000, 0.000000000000000000 ) ) ;
#414=EDGE_CURVE ( 'NONE', #9650, #2266, #7804, .T. ) ;
#417=VECTOR ( 'NONE', #1476, 1000.000000000000000 ) ;
#419=DIRECTION ( 'NONE',  ( 0.000000000000000000, -1.000000000000000000, 0.000000000000000000 ) ) ;
#421=ORIENTED_EDGE ( 'NONE', *, *, #5238, .T. ) ;
#424=CARTESIAN_POINT ( 'NONE',  ( 24.68830583033274806, -7.750000000000000000, 0.000000000000000000 ) ) ;
#431=CLOSED_SHELL ( 'NONE', ( #277, #9320, #9927, #8544, #10006, #399, #1911, #4446, #4671, #3762, #3426, #6874, #8625, #5452, #9045, #8690, #8125, #8773, #8910, #5128, #6954, #10114, #5058, #2205, #9564, #9977, #1593, #7544, #2557, #5719, #3320, #1896, #7278, #3681, #8319, #8899, #7533, #8941, #656, #771, #3259, #5912, #5057, #6064, #1527, #3579, #3527, #6993, #3388, #6405, #6791, #4611, #9290, #4035, #3186, #8628, #7763, #9179, #6201, #2777, #9603, #9417, #4009, #8640, #7128, #6228, #7169, #7521, #2767, #3637, #9890, #5832, #6553, #19, #1886, #7903, #7446, #7575 ) ) ;
#433=LINE ( 'NONE', #9391, #1094 ) ;
#436=CARTESIAN_POINT ( 'NONE',  ( 0.000000000000000000, 0.000000000000000000, 0.000000000000000000 ) ) ;
#441=PLANE ( 'NONE',  #10403 ) ;
#443=ORIENTED_EDGE ( 'NONE', *, *, #1753, .F. ) ;
#445=CARTESIAN_POINT ( 'NONE',  ( 25.00000000000000000, -4.000000000000000000, -2.000000000000000000 ) ) ;
#446=DIRECTION ( 'NONE',  ( 0.000000000000000000, 0.000000000000000000, 1.000000000000000000 ) ) ;
#449=ORIENTED_EDGE ( 'NONE', *, *, #6016, .F. ) ;
#453=ORIENTED_EDGE ( 'NONE', *, *, #3517, .T. ) ;
#456=LINE ( 'NONE', #10272, #519 ) ;
#457=EDGE_CURVE ( 'NONE', #3542, #5749, #6891, .T. ) ;
#463=ORIENTED_EDGE ( 'NONE', *, *, #6523, .F. ) ;
#466=SHAPE_REPRESENTATION_RELATIONSHIP ( 'NONE' , 'NONE' ,  #1027, #2591 ) ;
#468=EDGE_CURVE ( 'NONE', #1004, #5848, #10298, .T. ) ;
#469=CARTESIAN_POINT ( 'NONE',  ( 14.44459485323380754, -10.00000000000000000, -12.00000000000000000 ) ) ;
#472=EDGE_LOOP ( 'NONE', ( #8048, #6430, #5016, #6491 ) ) ;
#473=DIRECTION ( 'NONE',  ( 0.000000000000000000, 0.000000000000000000, 1.000000000000000000 ) ) ;
#481=CARTESIAN_POINT ( 'NONE',  ( 24.68830583033274806, -7.750000000000000000, -12.00000000000000000 ) ) ;
#485=DIRECTION ( 'NONE',  ( 0.000000000000000000, 1.000000000000000000, 0.000000000000000000 ) ) ;
#490=ORIENTED_EDGE ( 'NONE', *, *, #297, .F. ) ;
#493=DIRECTION ( 'NONE',  ( 0.9396926207859105373, -0.3420201433256627732, 0.000000000000000000 ) ) ;
#497=ORIENTED_EDGE ( 'NONE', *, *, #4647, .F. ) ;
#503=AXIS2_PLACEMENT_3D ( 'NONE', #6182, #6020, #7784 ) ;
#504=CARTESIAN_POINT ( 'NONE',  ( 20.72778015323380885, -10.00000000000000000, -12.00000000000000000 ) ) ;
#507=LINE ( 'NONE', #562, #3552 ) ;
#509=CARTESIAN_POINT ( 'NONE',  ( 23.26376179071655770, -10.02539999999999942, -12.00000000000000000 ) ) ;
#515=ORIENTED_EDGE ( 'NONE', *, *, #3261, .T. ) ;
#519=VECTOR ( 'NONE', #4424, 1000.000000000000000 ) ;
#521=LINE ( 'NONE', #3697, #2869 ) ;
#526=DIRECTION ( 'NONE',  ( 1.000000000000000000, 0.000000000000000000, 0.000000000000000000 ) ) ;
#528=VECTOR ( 'NONE', #619, 1000.000000000000000 ) ;
#535=DIRECTION ( 'NONE',  ( 0.3420201433256627732, -0.9396926207859105373, 0.000000000000000000 ) ) ;
#538=CARTESIAN_POINT ( 'NONE',  ( 12.75489823682933554, -14.64240329930025375, 0.000000000000000000 ) ) ;
#545=CARTESIAN_POINT ( 'NONE',  ( 25.57717656966725883, 3.750000000000000000, 0.000000000000000000 ) ) ;
#546=LINE ( 'NONE', #4618, #6946 ) ;
#547=PLANE ( 'NONE',  #4834 ) ;
#548=DIRECTION ( 'NONE',  ( 0.000000000000000000, -1.000000000000000000, -0.000000000000000000 ) ) ;
#549=ORIENTED_EDGE ( 'NONE', *, *, #5107, .F. ) ;
#550=DIRECTION ( 'NONE',  ( -1.000000000000000000, 0.000000000000000000, -0.000000000000000000 ) ) ;
#551=DIRECTION ( 'NONE',  ( 1.000000000000000000, -0.000000000000000000, -0.000000000000000000 ) ) ;
#552=EDGE_CURVE ( 'NONE', #7942, #3477, #1651, .T. ) ;
#562=CARTESIAN_POINT ( 'NONE',  ( 0.000000000000000000, -4.000000000000000000, -12.00000000000000000 ) ) ;
#567=EDGE_CURVE ( 'NONE', #10377, #9650, #8751, .T. ) ;
#568=ORIENTED_EDGE ( 'NONE', *, *, #8763, .F. ) ;
#572=LINE ( 'NONE', #4540, #9658 ) ;
#574=CARTESIAN_POINT ( 'NONE',  ( 6.727620669667255804, -7.750000000000000000, -12.00000000000000000 ) ) ;
#577=ORIENTED_EDGE ( 'NONE', *, *, #6674, .F. ) ;
#578=CARTESIAN_POINT ( 'NONE',  ( 16.15239861966725599, 3.750000000000000000, 0.000000000000000000 ) ) ;
#579=FACE_OUTER_BOUND ( 'NONE', #5973, .T. ) ;
#584=LINE ( 'NONE', #9284, #1451 ) ;
#589=ORIENTED_EDGE ( 'NONE', *, *, #10211, .F. ) ;
#593=EDGE_LOOP ( 'NONE', ( #8949, #9485, #3178, #7480 ) ) ;
#594=LINE ( 'NONE', #3827, #4076 ) ;
#596=CARTESIAN_POINT ( 'NONE',  ( 25.00000000000000000, -4.000000000000000000, 0.000000000000000000 ) ) ;
#599=CARTESIAN_POINT ( 'NONE',  ( 4.414205890716556446, 6.025400000000000311, -12.00000000000000000 ) ) ;
#600=ORIENTED_EDGE ( 'NONE', *, *, #5420, .T. ) ;
#602=LINE ( 'NONE', #4677, #9302 ) ;
#604=VECTOR ( 'NONE', #3880, 1000.000000000000000 ) ;
#609=ORIENTED_EDGE ( 'NONE', *, *, #2076, .T. ) ;
#613=CARTESIAN_POINT ( 'NONE',  ( 0.000000000000000000, -4.000000000000000000, -12.00000000000000000 ) ) ;
#614=VERTEX_POINT ( 'NONE', #9666 ) ;
#616=LINE ( 'NONE', #5484, #9988 ) ;
#618=VERTEX_POINT ( 'NONE', #10411 ) ;
#619=DIRECTION ( 'NONE',  ( 1.000000000000000000, -0.000000000000000000, -0.000000000000000000 ) ) ;
#621=ORIENTED_EDGE ( 'NONE', *, *, #4647, .T. ) ;
#624=DIRECTION ( 'NONE',  ( 0.9396926207859105373, 0.3420201433256627732, 0.000000000000000000 ) ) ;
#625=ORIENTED_EDGE ( 'NONE', *, *, #5895, .F. ) ;
#628=EDGE_CURVE ( 'NONE', #4280, #1390, #7154, .T. ) ;
#634=CARTESIAN_POINT ( 'NONE',  ( 0.000000000000000000, -10.00000000000000000, -12.00000000000000000 ) ) ;
#641=CARTESIAN_POINT ( 'NONE',  ( 16.15239861966725599, -7.750000000000000000, -12.00000000000000000 ) ) ;
#643=EDGE_LOOP ( 'NONE', ( #2365, #568, #1143, #6976 ) ) ;
#649=DIRECTION ( 'NONE',  ( 0.3420201433256627732, 0.9396926207859105373, 0.000000000000000000 ) ) ;
#656=ADVANCED_FACE ( 'NONE', ( #4031 ), #3184, .F. ) ;
#658=EDGE_LOOP ( 'NONE', ( #8231, #8896, #2249, #3731 ) ) ;
#660=CARTESIAN_POINT ( 'NONE',  ( 25.00000000000000000, -7.750000000000000000, -12.00000000000000000 ) ) ;
#666=DIRECTION ( 'NONE',  ( -1.000000000000000000, 0.000000000000000000, 0.000000000000000000 ) ) ;
#680=CARTESIAN_POINT ( 'NONE',  ( 21.54671318033274829, -7.750000000000000000, -12.00000000000000000 ) ) ;
#684=VECTOR ( 'NONE', #1145, 1000.000000000000000 ) ;
#694=DIRECTION ( 'NONE',  ( 0.000000000000000000, 0.000000000000000000, 1.000000000000000000 ) ) ;
#703=LINE ( 'NONE', #3932, #906 ) ;
#705=EDGE_CURVE ( 'NONE', #1471, #10128, #9772, .T. ) ;
#707=DIRECTION ( 'NONE',  ( 0.000000000000000000, 0.000000000000000000, -1.000000000000000000 ) ) ;
#711=CARTESIAN_POINT ( 'NONE',  ( 0.000000000000000000, -10.00000000000000000, 0.000000000000000000 ) ) ;
#717=VERTEX_POINT ( 'NONE', #2500 ) ;
#719=CARTESIAN_POINT ( 'NONE',  ( 10.68814634676619590, -10.00000000000000000, -12.00000000000000000 ) ) ;
#722=DIRECTION ( 'NONE',  ( -0.3420201433256627732, 0.9396926207859105373, 0.000000000000000000 ) ) ;
#731=CARTESIAN_POINT ( 'NONE',  ( 0.000000000000000000, -4.000000000000000000, -10.00000000000000000 ) ) ;
#742=DIRECTION ( 'NONE',  ( 0.000000000000000000, -1.000000000000000000, -0.000000000000000000 ) ) ;
#744=CARTESIAN_POINT ( 'NONE',  ( 0.4444353696672553311, -7.750000000000000000, -12.00000000000000000 ) ) ;
#747=VECTOR ( 'NONE', #5775, 1000.000000000000000 ) ;
#752=ORIENTED_EDGE ( 'NONE', *, *, #63, .T. ) ;
#760=ORIENTED_EDGE ( 'NONE', *, *, #6615, .F. ) ;
#771=ADVANCED_FACE ( 'NONE', ( #2069 ), #4745, .T. ) ;
#777=VECTOR ( 'NONE', #1134, 1000.000000000000000 ) ;
#782=ORIENTED_EDGE ( 'NONE', *, *, #6286, .F. ) ;
#784=EDGE_CURVE ( 'NONE', #614, #8730, #616, .T. ) ;
#785=EDGE_LOOP ( 'NONE', ( #7570, #6158, #4302, #1621 ) ) ;
#789=VERTEX_POINT ( 'NONE', #424 ) ;
#791=LINE ( 'NONE', #6345, #391 ) ;
#793=ORIENTED_EDGE ( 'NONE', *, *, #10301, .T. ) ;
#796=EDGE_CURVE ( 'NONE', #10128, #1894, #6384, .T. ) ;
#799=LINE ( 'NONE', #5612, #2459 ) ;
#809=DIRECTION ( 'NONE',  ( 0.000000000000000000, 0.000000000000000000, -1.000000000000000000 ) ) ;
#812=CARTESIAN_POINT ( 'NONE',  ( 17.57694265928344635, 6.025400000000000311, -12.00000000000000000 ) ) ;
#814=CARTESIAN_POINT ( 'NONE',  ( 7.555798540716556211, 6.025400000000000311, 0.000000000000000000 ) ) ;
#816=LINE ( 'NONE', #2514, #6764 ) ;
#821=ORIENTED_EDGE ( 'NONE', *, *, #2159, .T. ) ;
#827=ORIENTED_EDGE ( 'NONE', *, *, #925, .F. ) ;
#831=ORIENTED_EDGE ( 'NONE', *, *, #5642, .T. ) ;
#833=EDGE_LOOP ( 'NONE', ( #2518, #4015, #6107, #8146 ) ) ;
#842=ORIENTED_EDGE ( 'NONE', *, *, #902, .F. ) ;
#845=EDGE_CURVE ( 'NONE', #1584, #1356, #4688, .T. ) ;
#857=ORIENTED_EDGE ( 'NONE', *, *, #902, .T. ) ;
#858=VECTOR ( 'NONE', #1332, 1000.000000000000000 ) ;
#865=VECTOR ( 'NONE', #4833, 1000.000000000000000 ) ;
#866=CARTESIAN_POINT ( 'NONE',  ( 22.43558391966725907, 3.750000000000000000, 0.000000000000000000 ) ) ;
#872=LINE ( 'NONE', #1720, #1339 ) ;
#874=EDGE_CURVE ( 'NONE', #6381, #8915, #7129, .T. ) ;
#876=LINE ( 'NONE', #8034, #6940 ) ;
#878=VECTOR ( 'NONE', #10387, 1000.000000000000000 ) ;
#886=DIRECTION ( 'NONE',  ( 0.000000000000000000, 0.000000000000000000, 1.000000000000000000 ) ) ;
#892=DIRECTION ( 'NONE',  ( 0.3420201433256627732, -0.9396926207859105373, 0.000000000000000000 ) ) ;
#895=DIRECTION ( 'NONE',  ( 0.000000000000000000, 0.000000000000000000, -1.000000000000000000 ) ) ;
#901=PLANE ( 'NONE',  #7537 ) ;
#902=EDGE_CURVE ( 'NONE', #6552, #3003, #8535, .T. ) ;
#906=VECTOR ( 'NONE', #6253, 1000.000000000000000 ) ;
#909=VERTEX_POINT ( 'NONE', #6329 ) ;
#912=DIRECTION ( 'NONE',  ( 0.000000000000000000, -1.000000000000000000, -0.000000000000000000 ) ) ;
#917=DIRECTION ( 'NONE',  ( 0.000000000000000000, 0.000000000000000000, 1.000000000000000000 ) ) ;
#918=CARTESIAN_POINT ( 'NONE',  ( 20.71853530928344611, -10.02539999999999942, -12.00000000000000000 ) ) ;
#924=EDGE_LOOP ( 'NONE', ( #2423, #8115, #5753, #6912 ) ) ;
#925=EDGE_CURVE ( 'NONE', #10163, #2302, #9097, .T. ) ;
#928=VERTEX_POINT ( 'NONE', #1628 ) ;
#929=DIRECTION ( 'NONE',  ( 1.000000000000000000, 0.000000000000000000, 0.000000000000000000 ) ) ;
#930=LINE ( 'NONE', #4159, #5259 ) ;
#931=VERTEX_POINT ( 'NONE', #5011 ) ;
#934=CARTESIAN_POINT ( 'NONE',  ( 0.000000000000000000, -10.00000000000000000, -12.00000000000000000 ) ) ;
#939=EDGE_LOOP ( 'NONE', ( #6703, #4676, #5220, #5851 ) ) ;
#944=DIRECTION ( 'NONE',  ( 0.000000000000000000, 0.000000000000000000, 1.000000000000000000 ) ) ;
#946=VERTEX_POINT ( 'NONE', #7347 ) ;
#952=LINE ( 'NONE', #7413, #2229 ) ;
#955=CARTESIAN_POINT ( 'NONE',  ( 7.555798540716556211, 6.025400000000000311, -12.00000000000000000 ) ) ;
#957=CARTESIAN_POINT ( 'NONE',  ( 23.86012795928344588, -10.02539999999999942, -12.00000000000000000 ) ) ;
#965=CARTESIAN_POINT ( 'NONE',  ( 8.161409553233804459, -10.00000000000000000, -12.00000000000000000 ) ) ;
#969=CARTESIAN_POINT ( 'NONE',  ( 25.00000000000000000, 0.000000000000000000, -12.00000000000000000 ) ) ;
#976=ORIENTED_EDGE ( 'NONE', *, *, #6674, .T. ) ;
#979=CARTESIAN_POINT ( 'NONE',  ( 20.71853530928344611, 6.025400000000000311, -12.00000000000000000 ) ) ;
#985=EDGE_CURVE ( 'NONE', #6306, #614, #8305, .T. ) ;
#995=ORIENTED_EDGE ( 'NONE', *, *, #4802, .T. ) ;
#996=EDGE_CURVE ( 'NONE', #4979, #2729, #8356, .T. ) ;
#1000=ORIENTED_EDGE ( 'NONE', *, *, #9190, .T. ) ;
#1003=DIRECTION ( 'NONE',  ( 0.3420201433256627732, 0.9396926207859105373, 0.000000000000000000 ) ) ;
#1004=VERTEX_POINT ( 'NONE', #6263 ) ;
#1016=VECTOR ( 'NONE', #8993, 1000.000000000000000 ) ;
#1022=EDGE_CURVE ( 'NONE', #7942, #6026, #2940, .T. ) ;
#1026=ORIENTED_EDGE ( 'NONE', *, *, #8738, .F. ) ;
#1027=SHAPE_REPRESENTATION ( 'rack_ISO - Rack-spur - rectangular 1M 20PA 12FW 5PH 25L---SAll', ( #2101 ), #8215 ) ;
#1034=DIRECTION ( 'NONE',  ( -0.9396926207859105373, -0.3420201433256627732, 0.000000000000000000 ) ) ;
#1036=CARTESIAN_POINT ( 'NONE',  ( 5.838749930332745919, 3.750000000000000000, -12.00000000000000000 ) ) ;
#1037=VECTOR ( 'NONE', #7003, 1000.000000000000000 ) ;
#1043=ORIENTED_EDGE ( 'NONE', *, *, #4936, .F. ) ;
#1045=ORIENTED_EDGE ( 'NONE', *, *, #3799, .F. ) ;
#1057=EDGE_CURVE ( 'NONE', #7824, #1146, #602, .T. ) ;
#1059=EDGE_CURVE ( 'NONE', #4252, #2255, #10372, .T. ) ;
#1060=LINE ( 'NONE', #9872, #9831 ) ;
#1065=ORIENTED_EDGE ( 'NONE', *, *, #5251, .F. ) ;
#1066=DIRECTION ( 'NONE',  ( 0.3420201433256627732, -0.9396926207859105373, 0.000000000000000000 ) ) ;
#1067=PLANE ( 'NONE',  #1259 ) ;
#1068=CARTESIAN_POINT ( 'NONE',  ( 6.727620669667255804, 3.750000000000000000, -12.00000000000000000 ) ) ;
#1071=VECTOR ( 'NONE', #1221, 1000.000000000000000 ) ;
#1083=FACE_OUTER_BOUND ( 'NONE', #3328, .T. ) ;
#1084=ORIENTED_EDGE ( 'NONE', *, *, #6222, .F. ) ;
#1093=DIRECTION ( 'NONE',  ( 0.3420201433256627732, 0.9396926207859105373, 0.000000000000000000 ) ) ;
#1094=VECTOR ( 'NONE', #2863, 1000.000000000000000 ) ;
#1096=VERTEX_POINT ( 'NONE', #4727 ) ;
#1102=VECTOR ( 'NONE', #3758, 1000.000000000000000 ) ;
#1116=DIRECTION ( 'NONE',  ( 0.3420201433256627732, 0.9396926207859105373, -0.000000000000000000 ) ) ;
#1121=AXIS2_PLACEMENT_3D ( 'NONE', #9084, #5777, #4345 ) ;
#1124=PLANE ( 'NONE',  #9242 ) ;
#1134=DIRECTION ( 'NONE',  ( -1.000000000000000000, 0.000000000000000000, -0.000000000000000000 ) ) ;
#1135=LINE ( 'NONE', #8453, #8483 ) ;
#1138=FACE_OUTER_BOUND ( 'NONE', #7007, .T. ) ;
#1140=CARTESIAN_POINT ( 'NONE',  ( 7.546553696766195252, 6.000000000000000000, 0.000000000000000000 ) ) ;
#1143=ORIENTED_EDGE ( 'NONE', *, *, #9914, .T. ) ;
#1144=CARTESIAN_POINT ( 'NONE',  ( 25.00000000000000000, 0.000000000000000000, 0.000000000000000000 ) ) ;
#1145=DIRECTION ( 'NONE',  ( 1.000000000000000000, 0.000000000000000000, 0.000000000000000000 ) ) ;
#1146=VERTEX_POINT ( 'NONE', #3354 ) ;
#1155=DIRECTION ( 'NONE',  ( 1.000000000000000000, 0.000000000000000000, 0.000000000000000000 ) ) ;
#1156=ORIENTED_EDGE ( 'NONE', *, *, #6616, .T. ) ;
#1157=DIRECTION ( 'NONE',  ( -0.000000000000000000, -0.000000000000000000, 1.000000000000000000 ) ) ;
#1158=EDGE_CURVE ( 'NONE', #6291, #5295, #5727, .T. ) ;
#1163=DIRECTION ( 'NONE',  ( 0.3420201433256627732, 0.9396926207859105373, -0.000000000000000000 ) ) ;
#1164=VECTOR ( 'NONE', #3927, 1000.000000000000000 ) ;
#1168=DIRECTION ( 'NONE',  ( 0.3420201433256627732, -0.9396926207859105373, 0.000000000000000000 ) ) ;
#1171=EDGE_CURVE ( 'NONE', #1096, #1785, #5782, .T. ) ;
#1173=LINE ( 'NONE', #9286, #171 ) ;
#1175=VECTOR ( 'NONE', #4384, 1000.000000000000000 ) ;
#1183=EDGE_CURVE ( 'NONE', #1730, #9404, #8033, .T. ) ;
#1190=VECTOR ( 'NONE', #3780, 1000.000000000000000 ) ;
#1198=LINE ( 'NONE', #6752, #3147 ) ;
#1205=AXIS2_PLACEMENT_3D ( 'NONE', #8466, #2153, #4579 ) ;
#1212=CARTESIAN_POINT ( 'NONE',  ( 14.43535000928344481, 6.025400000000000311, -12.00000000000000000 ) ) ;
#1219=ORIENTED_EDGE ( 'NONE', *, *, #150, .T. ) ;
#1221=DIRECTION ( 'NONE',  ( 0.3420201433256627732, -0.9396926207859105373, 0.000000000000000000 ) ) ;
#1226=FACE_OUTER_BOUND ( 'NONE', #924, .T. ) ;
#1235=DIRECTION ( 'NONE',  ( 1.000000000000000000, 0.000000000000000000, 0.000000000000000000 ) ) ;
#1238=CARTESIAN_POINT ( 'NONE',  ( 20.11292429676619520, 6.000000000000000000, 0.000000000000000000 ) ) ;
#1258=DIRECTION ( 'NONE',  ( 0.000000000000000000, 0.000000000000000000, 1.000000000000000000 ) ) ;
#1259=AXIS2_PLACEMENT_3D ( 'NONE', #3503, #5874, #1970 ) ;
#1266=CARTESIAN_POINT ( 'NONE',  ( 10.68814634676619590, 6.000000000000000000, -12.00000000000000000 ) ) ;
#1269=ORIENTED_EDGE ( 'NONE', *, *, #2149, .F. ) ;
#1273=LINE ( 'NONE', #8489, #1071 ) ;
#1277=LINE ( 'NONE', #10141, #1102 ) ;
#1278=CARTESIAN_POINT ( 'NONE',  ( 11.30300220323380600, 6.000000000000000000, -12.00000000000000000 ) ) ;
#1279=PLANE ( 'NONE',  #6189 ) ;
#1292=EDGE_CURVE ( 'NONE', #2419, #2608, #8875, .T. ) ;
#1301=ORIENTED_EDGE ( 'NONE', *, *, #8334, .T. ) ;
#1308=ORIENTED_EDGE ( 'NONE', *, *, #5322, .T. ) ;
#1320=PLANE ( 'NONE',  #7513 ) ;
#1324=FACE_OUTER_BOUND ( 'NONE', #5872, .T. ) ;
#1332=DIRECTION ( 'NONE',  ( 1.000000000000000000, -0.000000000000000000, -0.000000000000000000 ) ) ;
#1339=VECTOR ( 'NONE', #8032, 1000.000000000000000 ) ;
#1343=AXIS2_PLACEMENT_3D ( 'NONE', #2447, #59, #5 ) ;
#1345=VECTOR ( 'NONE', #7183, 1000.000000000000000 ) ;
#1347=VERTEX_POINT ( 'NONE', #8075 ) ;
#1352=CARTESIAN_POINT ( 'NONE',  ( 19.29399126966725575, -7.750000000000000000, 0.000000000000000000 ) ) ;
#1354=AXIS2_PLACEMENT_3D ( 'NONE', #3708, #3924, #6297 ) ;
#1356=VERTEX_POINT ( 'NONE', #4034 ) ;
#1357=PLANE ( 'NONE',  #1549 ) ;
#1358=MECHANICAL_DESIGN_GEOMETRIC_PRESENTATION_REPRESENTATION('',(#2040),#4064);
#1361=ORIENTED_EDGE ( 'NONE', *, *, #9230, .F. ) ;
#1364=LINE ( 'NONE', #1212, #4308 ) ;
#1370=DIRECTION ( 'NONE',  ( 0.000000000000000000, 0.000000000000000000, -1.000000000000000000 ) ) ;
#1378=DIRECTION ( 'NONE',  ( 0.000000000000000000, 0.000000000000000000, -1.000000000000000000 ) ) ;
#1379=EDGE_CURVE ( 'NONE', #1396, #3111, #5667, .T. ) ;
#1381=PLANE ( 'NONE',  #8477 ) ;
#1388=EDGE_CURVE ( 'NONE', #3335, #7067, #7375, .T. ) ;
#1390=VERTEX_POINT ( 'NONE', #3343 ) ;
#1393=CARTESIAN_POINT ( 'NONE',  ( 0.4444353696672553311, 3.750000000000000000, -12.00000000000000000 ) ) ;
#1396=VERTEX_POINT ( 'NONE', #1553 ) ;
#1402=VERTEX_POINT ( 'NONE', #9022 ) ;
#1406=ORIENTED_EDGE ( 'NONE', *, *, #874, .T. ) ;
#1408=DIRECTION ( 'NONE',  ( 0.3420201433256627732, 0.9396926207859105373, -0.000000000000000000 ) ) ;
#1411=CARTESIAN_POINT ( 'NONE',  ( 0.000000000000000000, 6.000000000000000000, -12.00000000000000000 ) ) ;
#1416=ORIENTED_EDGE ( 'NONE', *, *, #6395, .F. ) ;
#1417=CARTESIAN_POINT ( 'NONE',  ( 13.83898384071655840, -10.02539999999999942, -12.00000000000000000 ) ) ;
#1419=ORIENTED_EDGE ( 'NONE', *, *, #7389, .T. ) ;
#1420=LINE ( 'NONE', #3750, #9991 ) ;
#1421=LINE ( 'NONE', #4762, #5297 ) ;
#1436=EDGE_CURVE ( 'NONE', #1390, #6164, #3986, .T. ) ;
#1437=EDGE_CURVE ( 'NONE', #4979, #4426, #6627, .T. ) ;
#1444=CARTESIAN_POINT ( 'NONE',  ( 0.000000000000000000, 6.000000000000000000, -12.00000000000000000 ) ) ;
#1446=CARTESIAN_POINT ( 'NONE',  ( 1.272613240716556016, 6.025400000000000311, 0.000000000000000000 ) ) ;
#1451=VECTOR ( 'NONE', #8543, 1000.000000000000000 ) ;
#1452=DIRECTION ( 'NONE',  ( 0.3420201433256627732, 0.9396926207859105373, -0.000000000000000000 ) ) ;
#1462=DIRECTION ( 'NONE',  ( -0.3420201433256627732, -0.9396926207859105373, 0.000000000000000000 ) ) ;
#1467=ORIENTED_EDGE ( 'NONE', *, *, #1436, .F. ) ;
#1468=LINE ( 'NONE', #7186, #3238 ) ;
#1471=VERTEX_POINT ( 'NONE', #8437 ) ;
#1476=DIRECTION ( 'NONE',  ( -1.000000000000000000, -0.000000000000000000, -0.000000000000000000 ) ) ;
#1478=VERTEX_POINT ( 'NONE', #2610 ) ;
#1481=DIRECTION ( 'NONE',  ( -0.000000000000000000, 1.000000000000000000, 0.000000000000000000 ) ) ;
#1498=EDGE_CURVE ( 'NONE', #928, #4800, #4239, .T. ) ;
#1500=EDGE_CURVE ( 'NONE', #6214, #7824, #9077, .T. ) ;
#1501=LINE ( 'NONE', #4094, #4493 ) ;
#1503=LINE ( 'NONE', #3091, #5169 ) ;
#1504=DIRECTION ( 'NONE',  ( -0.3420201433256627732, 0.9396926207859105373, 0.000000000000000000 ) ) ;
#1521=PLANE ( 'NONE',  #10168 ) ;
#1526=ORIENTED_EDGE ( 'NONE', *, *, #2218, .F. ) ;
#1527=ADVANCED_FACE ( 'NONE', ( #7580 ), #323, .T. ) ;
#1528=EDGE_LOOP ( 'NONE', ( #256, #6979, #7037, #4795 ) ) ;
#1529=DIRECTION ( 'NONE',  ( 0.000000000000000000, 1.000000000000000000, 0.000000000000000000 ) ) ;
#1530=AXIS2_PLACEMENT_3D ( 'NONE', #6853, #1832, #8358 ) ;
#1534=LINE ( 'NONE', #8004, #6645 ) ;
#1537=VECTOR ( 'NONE', #10492, 1000.000000000000000 ) ;
#1547=DIRECTION ( 'NONE',  ( 0.000000000000000000, 0.000000000000000000, -1.000000000000000000 ) ) ;
#1548=LINE ( 'NONE', #2337, #4328 ) ;
#1549=AXIS2_PLACEMENT_3D ( 'NONE', #10072, #2060, #5285 ) ;
#1550=CARTESIAN_POINT ( 'NONE',  ( 22.43558391966725907, -7.750000000000000000, -12.00000000000000000 ) ) ;
#1552=ORIENTED_EDGE ( 'NONE', *, *, #4165, .T. ) ;
#1553=CARTESIAN_POINT ( 'NONE',  ( 25.00000000000000000, 0.000000000000000000, -2.000000000000000000 ) ) ;
#1554=VECTOR ( 'NONE', #5686, 1000.000000000000000 ) ;
#1557=DIRECTION ( 'NONE',  ( 0.000000000000000000, -0.000000000000000000, 1.000000000000000000 ) ) ;
#1563=LINE ( 'NONE', #4787, #2890 ) ;
#1564=FACE_OUTER_BOUND ( 'NONE', #2785, .T. ) ;
#1569=UNCERTAINTY_MEASURE_WITH_UNIT (LENGTH_MEASURE( 1.000000000000000082E-05 ), #5698, 'distance_accuracy_value', 'NONE');
#1571=ORIENTED_EDGE ( 'NONE', *, *, #5320, .T. ) ;
#1573=LINE ( 'NONE', #8774, #3569 ) ;
#1574=LINE ( 'NONE', #3841, #2550 ) ;
#1580=EDGE_CURVE ( 'NONE', #4280, #2958, #9229, .T. ) ;
#1584=VERTEX_POINT ( 'NONE', #7530 ) ;
#1586=LINE ( 'NONE', #731, #97 ) ;
#1592=VERTEX_POINT ( 'NONE', #3502 ) ;
#1593=ADVANCED_FACE ( 'NONE', ( #4189 ), #1969, .F. ) ;
#1597=VERTEX_POINT ( 'NONE', #6830 ) ;
#1598=LINE ( 'NONE', #744, #5152 ) ;
#1611=DIRECTION ( 'NONE',  ( 0.000000000000000000, -0.000000000000000000, 1.000000000000000000 ) ) ;
#1615=CARTESIAN_POINT ( 'NONE',  ( 25.00000000000000000, -7.750000000000000000, -12.00000000000000000 ) ) ;
#1621=ORIENTED_EDGE ( 'NONE', *, *, #7477, .T. ) ;
#1624=EDGE_CURVE ( 'NONE', #909, #2796, #167, .T. ) ;
#1628=CARTESIAN_POINT ( 'NONE',  ( 16.15239861966725599, 3.750000000000000000, 0.000000000000000000 ) ) ;
#1634=ORIENTED_EDGE ( 'NONE', *, *, #9019, .F. ) ;
#1635=EDGE_CURVE ( 'NONE', #1592, #6214, #5448, .T. ) ;
#1643=VERTEX_POINT ( 'NONE', #2969 ) ;
#1649=CARTESIAN_POINT ( 'NONE',  ( 17.58618750323380908, -10.00000000000000000, -12.00000000000000000 ) ) ;
#1651=LINE ( 'NONE', #4710, #4829 ) ;
#1653=ORIENTED_EDGE ( 'NONE', *, *, #567, .F. ) ;
#1654=DIRECTION ( 'NONE',  ( -1.000000000000000000, 0.000000000000000000, 0.000000000000000000 ) ) ;
#1658=EDGE_CURVE ( 'NONE', #618, #928, #5394, .T. ) ;
#1660=PLANE ( 'NONE',  #3811 ) ;
#1661=CARTESIAN_POINT ( 'NONE',  ( 14.43535000928344481, -10.02539999999999942, -12.00000000000000000 ) ) ;
#1662=LINE ( 'NONE', #7276, #3571 ) ;
#1664=DIRECTION ( 'NONE',  ( -0.3420201433256627732, -0.9396926207859105373, 0.000000000000000000 ) ) ;
#1670=ORIENTED_EDGE ( 'NONE', *, *, #287, .F. ) ;
#1672=FACE_OUTER_BOUND ( 'NONE', #8195, .T. ) ;
#1673=EDGE_CURVE ( 'NONE', #9650, #7351, #6237, .T. ) ;
#1678=EDGE_LOOP ( 'NONE', ( #3431, #3738, #89, #4935 ) ) ;
#1684=ORIENTED_EDGE ( 'NONE', *, *, #552, .T. ) ;
#1686=VECTOR ( 'NONE', #2465, 1000.000000000000000 ) ;
#1687=CARTESIAN_POINT ( 'NONE',  ( 18.40512053033274853, -7.750000000000000000, -12.00000000000000000 ) ) ;
#1689=VECTOR ( 'NONE', #1157, 1000.000000000000000 ) ;
#1691=FACE_OUTER_BOUND ( 'NONE', #2438, .T. ) ;
#1696=AXIS2_PLACEMENT_3D ( 'NONE', #7628, #3647, #9380 ) ;
#1700=CARTESIAN_POINT ( 'NONE',  ( 16.15239861966725599, -7.750000000000000000, 0.000000000000000000 ) ) ;
#1707=CARTESIAN_POINT ( 'NONE',  ( 25.00000000000000000, 0.000000000000000000, -2.000000000000000000 ) ) ;
#1718=PLANE ( 'NONE',  #6271 ) ;
#1720=CARTESIAN_POINT ( 'NONE',  ( 23.26376179071655770, 6.025400000000000311, 0.000000000000000000 ) ) ;
#1722=AXIS2_PLACEMENT_3D ( 'NONE', #8083, #1913, #5134 ) ;
#1726=ORIENTED_EDGE ( 'NONE', *, *, #21, .F. ) ;
#1727=ORIENTED_EDGE ( 'NONE', *, *, #3755, .T. ) ;
#1730=VERTEX_POINT ( 'NONE', #5346 ) ;
#1732=DIRECTION ( 'NONE',  ( 0.000000000000000000, 0.000000000000000000, 1.000000000000000000 ) ) ;
#1738=CARTESIAN_POINT ( 'NONE',  ( 19.29399126966725575, -7.750000000000000000, -12.00000000000000000 ) ) ;
#1739=SURFACE_SIDE_STYLE ('',( #4268 ) ) ;
#1744=VERTEX_POINT ( 'NONE', #9443 ) ;
#1748=LINE ( 'NONE', #955, #8553 ) ;
#1753=EDGE_CURVE ( 'NONE', #2266, #946, #4443, .T. ) ;
#1754=AXIS2_PLACEMENT_3D ( 'NONE', #7857, #8866, #1557 ) ;
#1767=EDGE_CURVE ( 'NONE', #2958, #9757, #952, .T. ) ;
#1768=CARTESIAN_POINT ( 'NONE',  ( 12.12193523033274545, 3.750000000000000000, -12.00000000000000000 ) ) ;
#1770=VECTOR ( 'NONE', #6028, 1000.000000000000000 ) ;
#1778=EDGE_CURVE ( 'NONE', #8159, #3937, #2902, .T. ) ;
#1779=CARTESIAN_POINT ( 'NONE',  ( 9.869213319667256457, -7.750000000000000000, 0.000000000000000000 ) ) ;
#1785=VERTEX_POINT ( 'NONE', #8578 ) ;
#1789=ORIENTED_EDGE ( 'NONE', *, *, #7459, .F. ) ;
#1792=FACE_OUTER_BOUND ( 'NONE', #939, .T. ) ;
#1799=AXIS2_PLACEMENT_3D ( 'NONE', #4449, #6195, #7698 ) ;
#1807=CARTESIAN_POINT ( 'NONE',  ( 1.272613240716556016, -10.02539999999999942, -12.00000000000000000 ) ) ;
#1811=ORIENTED_EDGE ( 'NONE', *, *, #9195, .F. ) ;
#1815=EDGE_CURVE ( 'NONE', #9178, #9951, #3791, .T. ) ;
#1818=CARTESIAN_POINT ( 'NONE',  ( 23.86937280323380506, 6.000000000000001776, -12.00000000000000000 ) ) ;
#1819=DIRECTION ( 'NONE',  ( 0.3420201433256627732, 0.9396926207859105373, 0.000000000000000000 ) ) ;
#1820=DIRECTION ( 'NONE',  ( 0.000000000000000000, -0.000000000000000000, -1.000000000000000000 ) ) ;
#1825=ORIENTED_EDGE ( 'NONE', *, *, #4857, .F. ) ;
#1832=DIRECTION ( 'NONE',  ( -1.000000000000000000, 0.000000000000000000, 0.000000000000000000 ) ) ;
#1839=ORIENTED_EDGE ( 'NONE', *, *, #3054, .F. ) ;
#1842=CARTESIAN_POINT ( 'NONE',  ( 2.697157280332745266, -7.750000000000000000, 0.000000000000000000 ) ) ;
#1844=ORIENTED_EDGE ( 'NONE', *, *, #5107, .T. ) ;
#1850=EDGE_CURVE ( 'NONE', #9178, #4330, #2161, .T. ) ;
#1852=VECTOR ( 'NONE', #886, 1000.000000000000000 ) ;
#1856=DIRECTION ( 'NONE',  ( -0.9396926207859105373, 0.3420201433256627732, 0.000000000000000000 ) ) ;
#1858=CARTESIAN_POINT ( 'NONE',  ( 23.26376179071655770, -10.02539999999999942, 0.000000000000000000 ) ) ;
#1862=ORIENTED_EDGE ( 'NONE', *, *, #2628, .T. ) ;
#1869=DIRECTION ( 'NONE',  ( 0.9396926207859105373, -0.3420201433256627732, 0.000000000000000000 ) ) ;
#1878=VECTOR ( 'NONE', #6081, 1000.000000000000000 ) ;
#1884=DIRECTION ( 'NONE',  ( 1.000000000000000000, -0.000000000000000000, -0.000000000000000000 ) ) ;
#1885=ORIENTED_EDGE ( 'NONE', *, *, #6222, .T. ) ;
#1886=ADVANCED_FACE ( 'NONE', ( #7778 ), #6175, .F. ) ;
#1887=DIRECTION ( 'NONE',  ( -0.000000000000000000, -0.000000000000000000, 1.000000000000000000 ) ) ;
#1888=AXIS2_PLACEMENT_3D ( 'NONE', #509, #8621, #9480 ) ;
#1892=ORIENTED_EDGE ( 'NONE', *, *, #6016, .T. ) ;
#1894=VERTEX_POINT ( 'NONE', #5381 ) ;
#1895=DIRECTION ( 'NONE',  ( -1.000000000000000000, -0.000000000000000000, -0.000000000000000000 ) ) ;
#1896=ADVANCED_FACE ( 'NONE', ( #2846 ), #1357, .F. ) ;
#1897=PLANE ( 'NONE',  #8642 ) ;
#1898=ORIENTED_EDGE ( 'NONE', *, *, #3463, .F. ) ;
#1906=( LENGTH_UNIT ( ) NAMED_UNIT ( * ) SI_UNIT ( .MILLI., .METRE. ) );
#1908=LINE ( 'NONE', #3336, #9063 ) ;
#1909=PLANE ( 'NONE',  #503 ) ;
#1910=ORIENTED_EDGE ( 'NONE', *, *, #1388, .F. ) ;
#1911=ADVANCED_FACE ( 'NONE', ( #5437 ), #5333, .T. ) ;
#1913=DIRECTION ( 'NONE',  ( -0.9396926207859105373, -0.3420201433256627732, 0.000000000000000000 ) ) ;
#1917=CARTESIAN_POINT ( 'NONE',  ( 13.83898384071655840, 6.025400000000000311, 0.000000000000000000 ) ) ;
#1923=PLANE ( 'NONE',  #6861 ) ;
#1933=DIRECTION ( 'NONE',  ( 0.3420201433256627732, 0.9396926207859105373, -0.000000000000000000 ) ) ;
#1935=EDGE_LOOP ( 'NONE', ( #2857, #2703, #8254, #2112 ) ) ;
#1946=VECTOR ( 'NONE', #7415, 1000.000000000000000 ) ;
#1951=CARTESIAN_POINT ( 'NONE',  ( 13.83898384071655840, 6.025400000000000311, -12.00000000000000000 ) ) ;
#1960=CARTESIAN_POINT ( 'NONE',  ( 10.68814634676619590, -10.00000000000000000, 0.000000000000000000 ) ) ;
#1961=ORIENTED_EDGE ( 'NONE', *, *, #2220, .T. ) ;
#1962=CARTESIAN_POINT ( 'NONE',  ( 0.000000000000000000, 6.000000000000000000, 0.000000000000000000 ) ) ;
#1967=EDGE_LOOP ( 'NONE', ( #7031, #8687, #5104, #4482 ) ) ;
#1969=PLANE ( 'NONE',  #8818 ) ;
#1970=DIRECTION ( 'NONE',  ( 0.3420201433256627732, 0.9396926207859105373, 0.000000000000000000 ) ) ;
#1975=VECTOR ( 'NONE', #7045, 1000.000000000000000 ) ;
#1976=CARTESIAN_POINT ( 'NONE',  ( 7.546553696766195252, -10.00000000000000000, 0.000000000000000000 ) ) ;
#1982=EDGE_CURVE ( 'NONE', #1996, #6164, #9642, .T. ) ;
#1986=CARTESIAN_POINT ( 'NONE',  ( 21.54671318033274829, -7.750000000000000000, 0.000000000000000000 ) ) ;
#1988=ORIENTED_EDGE ( 'NONE', *, *, #1379, .F. ) ;
#1991=EDGE_CURVE ( 'NONE', #1478, #8065, #1468, .T. ) ;
#1994=EDGE_LOOP ( 'NONE', ( #3224, #6584, #2790, #9112 ) ) ;
#1996=VERTEX_POINT ( 'NONE', #8839 ) ;
#2000=DIRECTION ( 'NONE',  ( 0.3420201433256627732, -0.9396926207859105373, 0.000000000000000000 ) ) ;
#2005=VERTEX_POINT ( 'NONE', #6387 ) ;
#2010=FACE_OUTER_BOUND ( 'NONE', #5588, .T. ) ;
#2014=CARTESIAN_POINT ( 'NONE',  ( 5.010572059283444624, -10.02539999999999942, -12.00000000000000000 ) ) ;
#2016=ORIENTED_EDGE ( 'NONE', *, *, #21, .T. ) ;
#2018=VECTOR ( 'NONE', #1408, 1000.000000000000000 ) ;
#2024=VECTOR ( 'NONE', #550, 1000.000000000000000 ) ;
#2029=EDGE_CURVE ( 'NONE', #4487, #3187, #5487, .T. ) ;
#2035=DIRECTION ( 'NONE',  ( 0.000000000000000000, 0.000000000000000000, 1.000000000000000000 ) ) ;
#2037=CARTESIAN_POINT ( 'NONE',  ( 0.000000000000000000, 6.000000000000000000, -12.00000000000000000 ) ) ;
#2040=STYLED_ITEM ( 'NONE', ( #5855 ), #7952 ) ;
#2048=VECTOR ( 'NONE', #3939, 1000.000000000000000 ) ;
#2052=VECTOR ( 'NONE', #8348, 1000.000000000000000 ) ;
#2060=DIRECTION ( 'NONE',  ( -0.9396926207859105373, -0.3420201433256627732, 0.000000000000000000 ) ) ;
#2062=FILL_AREA_STYLE ('',( #9321 ) ) ;
#2069=FACE_OUTER_BOUND ( 'NONE', #262, .T. ) ;
#2076=EDGE_CURVE ( 'NONE', #8065, #2419, #6898, .T. ) ;
#2077=DIRECTION ( 'NONE',  ( -0.000000000000000000, 1.000000000000000000, 0.000000000000000000 ) ) ;
#2078=CARTESIAN_POINT ( 'NONE',  ( 17.58618750323380908, -10.00000000000000000, 0.000000000000000000 ) ) ;
#2084=ORIENTED_EDGE ( 'NONE', *, *, #2149, .T. ) ;
#2088=EDGE_CURVE ( 'NONE', #6626, #9328, #2190, .T. ) ;
#2094=VECTOR ( 'NONE', #2230, 1000.000000000000000 ) ;
#2100=ORIENTED_EDGE ( 'NONE', *, *, #6786, .T. ) ;
#2101=AXIS2_PLACEMENT_3D ( 'NONE', #7090, #5610, #4547 ) ;
#2103=LINE ( 'NONE', #3584, #5082 ) ;
#2106=CARTESIAN_POINT ( 'NONE',  ( 0.000000000000000000, 6.000000000000000000, -12.00000000000000000 ) ) ;
#2110=ORIENTED_EDGE ( 'NONE', *, *, #3555, .T. ) ;
#2112=ORIENTED_EDGE ( 'NONE', *, *, #1436, .T. ) ;
#2114=STYLED_ITEM ( 'NONE', ( #8328 ), #2591 ) ;
#2115=DIRECTION ( 'NONE',  ( 1.000000000000000000, -0.000000000000000000, -0.000000000000000000 ) ) ;
#2123=CARTESIAN_POINT ( 'NONE',  ( 1.658513752677435171, 6.603649639095712232, 0.000000000000000000 ) ) ;
#2124=DIRECTION ( 'NONE',  ( 0.000000000000000000, 0.000000000000000000, -1.000000000000000000 ) ) ;
#2126=VECTOR ( 'NONE', #3583, 1000.000000000000000 ) ;
#2128=CARTESIAN_POINT ( 'NONE',  ( 22.43558391966725907, 3.750000000000000000, -12.00000000000000000 ) ) ;
#2129=EDGE_CURVE ( 'NONE', #1478, #1396, #2246, .T. ) ;
#2136=EDGE_CURVE ( 'NONE', #6924, #1347, #8602, .T. ) ;
#2140=ORIENTED_EDGE ( 'NONE', *, *, #4588, .T. ) ;
#2141=LINE ( 'NONE', #7653, #6437 ) ;
#2145=ORIENTED_EDGE ( 'NONE', *, *, #2586, .F. ) ;
#2147=CARTESIAN_POINT ( 'NONE',  ( 12.12193523033274545, -7.750000000000000000, -12.00000000000000000 ) ) ;
#2149=EDGE_CURVE ( 'NONE', #9328, #5890, #6155, .T. ) ;
#2153=DIRECTION ( 'NONE',  ( -0.9396926207859105373, -0.3420201433256627732, 0.000000000000000000 ) ) ;
#2158=ORIENTED_EDGE ( 'NONE', *, *, #2029, .F. ) ;
#2159=EDGE_CURVE ( 'NONE', #8622, #7022, #10153, .T. ) ;
#2161=LINE ( 'NONE', #10124, #528 ) ;
#2166=ORIENTED_EDGE ( 'NONE', *, *, #5697, .T. ) ;
#2167=CARTESIAN_POINT ( 'NONE',  ( 25.00000000000000000, 3.750000000000000000, -12.00000000000000000 ) ) ;
#2182=AXIS2_PLACEMENT_3D ( 'NONE', #6247, #485, #5404 ) ;
#2186=DIRECTION ( 'NONE',  ( 1.000000000000000000, 0.000000000000000000, 0.000000000000000000 ) ) ;
#2187=ORIENTED_EDGE ( 'NONE', *, *, #1580, .T. ) ;
#2190=LINE ( 'NONE', #1393, #8826 ) ;
#2192=CARTESIAN_POINT ( 'NONE',  ( 6.727620669667255804, -7.750000000000000000, -12.00000000000000000 ) ) ;
#2193=LINE ( 'NONE', #2248, #2048 ) ;
#2195=VECTOR ( 'NONE', #8873, 1000.000000000000000 ) ;
#2196=DIRECTION ( 'NONE',  ( 0.000000000000000000, 0.000000000000000000, -1.000000000000000000 ) ) ;
#2202=ORIENTED_EDGE ( 'NONE', *, *, #2609, .T. ) ;
#2205=ADVANCED_FACE ( 'NONE', ( #8659 ), #5468, .F. ) ;
#2206=CARTESIAN_POINT ( 'NONE',  ( 21.07718659994326060, -17.67146854445365989, 0.000000000000000000 ) ) ;
#2213=VERTEX_POINT ( 'NONE', #7816 ) ;
#2218=EDGE_CURVE ( 'NONE', #5749, #909, #546, .T. ) ;
#2220=EDGE_CURVE ( 'NONE', #618, #2377, #7055, .T. ) ;
#2229=VECTOR ( 'NONE', #154, 1000.000000000000000 ) ;
#2230=DIRECTION ( 'NONE',  ( -0.3420201433256627732, 0.9396926207859105373, 0.000000000000000000 ) ) ;
#2233=DIRECTION ( 'NONE',  ( -1.000000000000000000, 0.000000000000000000, -0.000000000000000000 ) ) ;
#2234=FACE_OUTER_BOUND ( 'NONE', #1528, .T. ) ;
#2236=FACE_OUTER_BOUND ( 'NONE', #7422, .T. ) ;
#2245=CARTESIAN_POINT ( 'NONE',  ( 0.4444353696672553311, 3.750000000000000000, -12.00000000000000000 ) ) ;
#2246=LINE ( 'NONE', #445, #2395 ) ;
#2247=DIRECTION ( 'NONE',  ( -1.000000000000000000, -0.000000000000000000, -0.000000000000000000 ) ) ;
#2248=CARTESIAN_POINT ( 'NONE',  ( 6.727620669667255804, 3.750000000000000000, 0.000000000000000000 ) ) ;
#2249=ORIENTED_EDGE ( 'NONE', *, *, #9736, .T. ) ;
#2253=ORIENTED_EDGE ( 'NONE', *, *, #6017, .T. ) ;
#2255=VERTEX_POINT ( 'NONE', #4977 ) ;
#2256=DIRECTION ( 'NONE',  ( 0.3420201433256627732, 0.9396926207859105373, 0.000000000000000000 ) ) ;
#2262=ORIENTED_EDGE ( 'NONE', *, *, #5783, .F. ) ;
#2266=VERTEX_POINT ( 'NONE', #3235 ) ;
#2271=ORIENTED_EDGE ( 'NONE', *, *, #9419, .F. ) ;
#2272=LINE ( 'NONE', #8584, #5572 ) ;
#2273=CARTESIAN_POINT ( 'NONE',  ( 0.000000000000000000, 6.000000000000000000, 0.000000000000000000 ) ) ;
#2276=VERTEX_POINT ( 'NONE', #6620 ) ;
#2277=CARTESIAN_POINT ( 'NONE',  ( 9.869213319667256457, -7.750000000000000000, 0.000000000000000000 ) ) ;
#2286=AXIS2_PLACEMENT_3D ( 'NONE', #9068, #6664, #9012 ) ;
#2293=FACE_OUTER_BOUND ( 'NONE', #9810, .T. ) ;
#2296=SHAPE_DEFINITION_REPRESENTATION ( #4871, #1027 ) ;
#2297=CARTESIAN_POINT ( 'NONE',  ( 1.272613240716556016, 6.025400000000000311, -12.00000000000000000 ) ) ;
#2298=DIRECTION ( 'NONE',  ( 0.000000000000000000, -1.000000000000000000, 0.000000000000000000 ) ) ;
#2299=ORIENTED_EDGE ( 'NONE', *, *, #784, .T. ) ;
#2302=VERTEX_POINT ( 'NONE', #3390 ) ;
#2312=ORIENTED_EDGE ( 'NONE', *, *, #6038, .T. ) ;
#2315=DIRECTION ( 'NONE',  ( -0.000000000000000000, 1.000000000000000000, -0.000000000000000000 ) ) ;
#2323=CARTESIAN_POINT ( 'NONE',  ( 0.000000000000000000, 6.000000000000000000, 0.000000000000000000 ) ) ;
#2327=DIRECTION ( 'NONE',  ( -0.000000000000000000, 0.000000000000000000, -1.000000000000000000 ) ) ;
#2337=CARTESIAN_POINT ( 'NONE',  ( 9.869213319667256457, 3.750000000000000000, -12.00000000000000000 ) ) ;
#2350=CARTESIAN_POINT ( 'NONE',  ( 0.4444353696672553311, -7.750000000000000000, -12.00000000000000000 ) ) ;
#2355=CARTESIAN_POINT ( 'NONE',  ( 16.15239861966725599, -7.750000000000000000, -12.00000000000000000 ) ) ;
#2363=LINE ( 'NONE', #2421, #5258 ) ;
#2365=ORIENTED_EDGE ( 'NONE', *, *, #9195, .T. ) ;
#2367=ORIENTED_EDGE ( 'NONE', *, *, #7400, .T. ) ;
#2377=VERTEX_POINT ( 'NONE', #2392 ) ;
#2381=ORIENTED_EDGE ( 'NONE', *, *, #5192, .F. ) ;
#2391=VECTOR ( 'NONE', #3951, 1000.000000000000000 ) ;
#2392=CARTESIAN_POINT ( 'NONE',  ( 14.44459485323380576, 6.000000000000000000, 0.000000000000000000 ) ) ;
#2394=DIRECTION ( 'NONE',  ( 0.9396926207859105373, 0.3420201433256627732, 0.000000000000000000 ) ) ;
#2395=VECTOR ( 'NONE', #7709, 1000.000000000000000 ) ;
#2398=VERTEX_POINT ( 'NONE', #5613 ) ;
#2408=ORIENTED_EDGE ( 'NONE', *, *, #468, .F. ) ;
#2416=EDGE_CURVE ( 'NONE', #6924, #6457, #2547, .T. ) ;
#2418=EDGE_CURVE ( 'NONE', #3874, #7594, #4769, .T. ) ;
#2419=VERTEX_POINT ( 'NONE', #9116 ) ;
#2421=CARTESIAN_POINT ( 'NONE',  ( 0.000000000000000000, -10.00000000000000000, -12.00000000000000000 ) ) ;
#2423=ORIENTED_EDGE ( 'NONE', *, *, #1850, .T. ) ;
#2425=CARTESIAN_POINT ( 'NONE',  ( 0.000000000000000000, 0.000000000000000000, -12.00000000000000000 ) ) ;
#2429=ORIENTED_EDGE ( 'NONE', *, *, #8334, .F. ) ;
#2434=ORIENTED_EDGE ( 'NONE', *, *, #4300, .T. ) ;
#2438=EDGE_LOOP ( 'NONE', ( #782, #1156, #10037, #224 ) ) ;
#2445=DIRECTION ( 'NONE',  ( 1.000000000000000000, 0.000000000000000000, 0.000000000000000000 ) ) ;
#2447=CARTESIAN_POINT ( 'NONE',  ( 20.12216914071655793, 6.025400000000000311, -12.00000000000000000 ) ) ;
#2448=VECTOR ( 'NONE', #2124, 1000.000000000000000 ) ;
#2452=ORIENTED_EDGE ( 'NONE', *, *, #3400, .T. ) ;
#2455=DIRECTION ( 'NONE',  ( 0.000000000000000000, 0.000000000000000000, -1.000000000000000000 ) ) ;
#2459=VECTOR ( 'NONE', #2233, 1000.000000000000000 ) ;
#2460=CARTESIAN_POINT ( 'NONE',  ( 21.07718659994326060, 13.67146854445365811, 0.000000000000000000 ) ) ;
#2463=LINE ( 'NONE', #5678, #8463 ) ;
#2465=DIRECTION ( 'NONE',  ( -1.000000000000000000, 0.000000000000000000, 0.000000000000000000 ) ) ;
#2467=VECTOR ( 'NONE', #5545, 1000.000000000000000 ) ;
#2470=EDGE_LOOP ( 'NONE', ( #2367, #5647, #3284, #2016 ) ) ;
#2473=LINE ( 'NONE', #243, #3233 ) ;
#2474=ORIENTED_EDGE ( 'NONE', *, *, #2136, .F. ) ;
#2478=PLANE ( 'NONE',  #6428 ) ;
#2479=EDGE_LOOP ( 'NONE', ( #4219, #4915, #9845, #10237 ) ) ;
#2485=ORIENTED_EDGE ( 'NONE', *, *, #1673, .T. ) ;
#2489=FACE_OUTER_BOUND ( 'NONE', #9905, .T. ) ;
#2500=CARTESIAN_POINT ( 'NONE',  ( 9.869213319667256457, -7.750000000000000000, -12.00000000000000000 ) ) ;
#2507=DIRECTION ( 'NONE',  ( 0.000000000000000000, 1.000000000000000000, 0.000000000000000000 ) ) ;
#2508=DIRECTION ( 'NONE',  ( 0.000000000000000000, 0.000000000000000000, -1.000000000000000000 ) ) ;
#2509=CARTESIAN_POINT ( 'NONE',  ( 3.586028019667255595, 3.750000000000000000, -12.00000000000000000 ) ) ;
#2511=LINE ( 'NONE', #918, #2195 ) ;
#2514=CARTESIAN_POINT ( 'NONE',  ( 13.01080596966725622, 3.750000000000000000, 0.000000000000000000 ) ) ;
#2516=LINE ( 'NONE', #5002, #3607 ) ;
#2518=ORIENTED_EDGE ( 'NONE', *, *, #4350, .F. ) ;
#2523=CARTESIAN_POINT ( 'NONE',  ( 0.000000000000000000, 0.000000000000000000, -12.00000000000000000 ) ) ;
#2525=VECTOR ( 'NONE', #3132, 1000.000000000000000 ) ;
#2531=ORIENTED_EDGE ( 'NONE', *, *, #6003, .F. ) ;
#2547=LINE ( 'NONE', #4182, #8651 ) ;
#2549=CARTESIAN_POINT ( 'NONE',  ( 10.69739119071655686, -10.02539999999999942, -12.00000000000000000 ) ) ;
#2550=VECTOR ( 'NONE', #1462, 1000.000000000000000 ) ;
#2553=ORIENTED_EDGE ( 'NONE', *, *, #203, .T. ) ;
#2557=ADVANCED_FACE ( 'NONE', ( #6665 ), #9922, .F. ) ;
#2558=CARTESIAN_POINT ( 'NONE',  ( 0.000000000000000000, -10.00000000000000000, 0.000000000000000000 ) ) ;
#2559=AXIS2_PLACEMENT_3D ( 'NONE', #2037, #3619, #8558 ) ;
#2573=ORIENTED_EDGE ( 'NONE', *, *, #4410, .T. ) ;
#2574=DIRECTION ( 'NONE',  ( 0.3420201433256627732, -0.9396926207859105373, 0.000000000000000000 ) ) ;
#2575=LINE ( 'NONE', #5790, #7631 ) ;
#2576=EDGE_LOOP ( 'NONE', ( #2888, #5204, #5800, #8674 ) ) ;
#2586=EDGE_CURVE ( 'NONE', #3324, #3111, #456, .T. ) ;
#2588=DIRECTION ( 'NONE',  ( -1.000000000000000000, -0.000000000000000000, -0.000000000000000000 ) ) ;
#2591=ADVANCED_BREP_SHAPE_REPRESENTATION ( '', ( #7952, #2101 ), #8215 ) ;
#2600=CARTESIAN_POINT ( 'NONE',  ( 6.727620669667255804, -7.750000000000000000, 0.000000000000000000 ) ) ;
#2601=DIRECTION ( 'NONE',  ( 0.3420201433256627732, -0.9396926207859105373, 0.000000000000000000 ) ) ;
#2604=VECTOR ( 'NONE', #8009, 1000.000000000000000 ) ;
#2608=VERTEX_POINT ( 'NONE', #660 ) ;
#2609=EDGE_CURVE ( 'NONE', #1584, #4442, #1573, .T. ) ;
#2610=CARTESIAN_POINT ( 'NONE',  ( 25.00000000000000000, -4.000000000000000000, -2.000000000000000000 ) ) ;
#2618=EDGE_CURVE ( 'NONE', #9748, #6164, #2363, .T. ) ;
#2628=EDGE_CURVE ( 'NONE', #3378, #9951, #7179, .T. ) ;
#2637=LINE ( 'NONE', #5750, #7200 ) ;
#2648=ORIENTED_EDGE ( 'NONE', *, *, #6651, .F. ) ;
#2658=DIRECTION ( 'NONE',  ( 0.000000000000000000, 0.000000000000000000, 1.000000000000000000 ) ) ;
#2670=VERTEX_POINT ( 'NONE', #6216 ) ;
#2671=EDGE_CURVE ( 'NONE', #7286, #7942, #9636, .T. ) ;
#2675=DIRECTION ( 'NONE',  ( 0.3420201433256627732, -0.9396926207859105373, 0.000000000000000000 ) ) ;
#2676=ORIENTED_EDGE ( 'NONE', *, *, #9614, .T. ) ;
#2686=CARTESIAN_POINT ( 'NONE',  ( 23.86937280323380506, -10.00000000000000178, 0.000000000000000000 ) ) ;
#2693=VECTOR ( 'NONE', #5458, 1000.000000000000000 ) ;
#2695=CARTESIAN_POINT ( 'NONE',  ( 25.00000000000000000, 0.000000000000000000, -10.00000000000000000 ) ) ;
#2698=ORIENTED_EDGE ( 'NONE', *, *, #150, .F. ) ;
#2703=ORIENTED_EDGE ( 'NONE', *, *, #4097, .F. ) ;
#2704=VECTOR ( 'NONE', #1155, 1000.000000000000000 ) ;
#2705=DIRECTION ( 'NONE',  ( 0.000000000000000000, 0.000000000000000000, 1.000000000000000000 ) ) ;
#2706=VECTOR ( 'NONE', #1732, 1000.000000000000000 ) ;
#2711=VECTOR ( 'NONE', #2588, 1000.000000000000000 ) ;
#2721=CARTESIAN_POINT ( 'NONE',  ( 22.43558391966725907, -7.750000000000000000, 0.000000000000000000 ) ) ;
#2726=CARTESIAN_POINT ( 'NONE',  ( 0.000000000000000000, -10.00000000000000000, 0.000000000000000000 ) ) ;
#2728=DIRECTION ( 'NONE',  ( 0.000000000000000000, 0.000000000000000000, -1.000000000000000000 ) ) ;
#2729=VERTEX_POINT ( 'NONE', #719 ) ;
#2736=VECTOR ( 'NONE', #8300, 1000.000000000000000 ) ;
#2742=CARTESIAN_POINT ( 'NONE',  ( 25.00000000000000000, 3.750000000000000000, -12.00000000000000000 ) ) ;
#2747=ORIENTED_EDGE ( 'NONE', *, *, #2816, .T. ) ;
#2751=DIRECTION ( 'NONE',  ( 0.000000000000000000, 0.000000000000000000, -1.000000000000000000 ) ) ;
#2752=CARTESIAN_POINT ( 'NONE',  ( 8.161409553233804459, 6.000000000000000000, -12.00000000000000000 ) ) ;
#2755=LINE ( 'NONE', #8923, #10185 ) ;
#2759=EDGE_CURVE ( 'NONE', #1744, #618, #8091, .T. ) ;
#2767=ADVANCED_FACE ( 'NONE', ( #8252 ), #8931, .F. ) ;
#2777=ADVANCED_FACE ( 'NONE', ( #5789 ), #6540, .F. ) ;
#2785=EDGE_LOOP ( 'NONE', ( #9422, #9659, #2187, #3100 ) ) ;
#2789=DIRECTION ( 'NONE',  ( 0.000000000000000000, 0.000000000000000000, 1.000000000000000000 ) ) ;
#2790=ORIENTED_EDGE ( 'NONE', *, *, #5642, .F. ) ;
#2796=VERTEX_POINT ( 'NONE', #1779 ) ;
#2800=ORIENTED_EDGE ( 'NONE', *, *, #2416, .F. ) ;
#2805=ORIENTED_EDGE ( 'NONE', *, *, #6723, .T. ) ;
#2807=VECTOR ( 'NONE', #6939, 1000.000000000000000 ) ;
#2809=DIRECTION ( 'NONE',  ( 1.000000000000000000, 0.000000000000000000, 0.000000000000000000 ) ) ;
#2816=EDGE_CURVE ( 'NONE', #4169, #6012, #5735, .T. ) ;
#2830=DIRECTION ( 'NONE',  ( 0.3420201433256627732, 0.9396926207859105373, 0.000000000000000000 ) ) ;
#2835=VERTEX_POINT ( 'NONE', #3312 ) ;
#2837=ORIENTED_EDGE ( 'NONE', *, *, #9217, .F. ) ;
#2845=EDGE_LOOP ( 'NONE', ( #5155, #8158, #55, #3121 ) ) ;
#2846=FACE_OUTER_BOUND ( 'NONE', #33, .T. ) ;
#2857=ORIENTED_EDGE ( 'NONE', *, *, #1982, .F. ) ;
#2859=EDGE_CURVE ( 'NONE', #789, #2419, #6641, .T. ) ;
#2863=DIRECTION ( 'NONE',  ( 0.3420201433256627732, 0.9396926207859105373, -0.000000000000000000 ) ) ;
#2865=CARTESIAN_POINT ( 'NONE',  ( 6.727620669667255804, 3.750000000000000000, 0.000000000000000000 ) ) ;
#2869=VECTOR ( 'NONE', #7032, 1000.000000000000000 ) ;
#2878=DIRECTION ( 'NONE',  ( -1.000000000000000000, 0.000000000000000000, -0.000000000000000000 ) ) ;
#2884=VECTOR ( 'NONE', #9351, 1000.000000000000000 ) ;
#2886=VECTOR ( 'NONE', #1116, 1000.000000000000000 ) ;
#2888=ORIENTED_EDGE ( 'NONE', *, *, #2029, .T. ) ;
#2890=VECTOR ( 'NONE', #3092, 1000.000000000000000 ) ;
#2902=LINE ( 'NONE', #10225, #31 ) ;
#2922=LINE ( 'NONE', #4605, #6089 ) ;
#2924=CARTESIAN_POINT ( 'NONE',  ( 0.000000000000000000, -10.00000000000000000, -12.00000000000000000 ) ) ;
#2931=VERTEX_POINT ( 'NONE', #1238 ) ;
#2938=FACE_OUTER_BOUND ( 'NONE', #7013, .T. ) ;
#2940=LINE ( 'NONE', #4570, #7603 ) ;
#2942=DIRECTION ( 'NONE',  ( 0.3420201433256627732, -0.9396926207859105373, 0.000000000000000000 ) ) ;
#2945=ORIENTED_EDGE ( 'NONE', *, *, #1624, .F. ) ;
#2946=ORIENTED_EDGE ( 'NONE', *, *, #4300, .F. ) ;
#2956=ORIENTED_EDGE ( 'NONE', *, *, #8576, .T. ) ;
#2958=VERTEX_POINT ( 'NONE', #1986 ) ;
#2968=VECTOR ( 'NONE', #2751, 1000.000000000000000 ) ;
#2969=CARTESIAN_POINT ( 'NONE',  ( 7.546553696766195252, -10.00000000000000000, -12.00000000000000000 ) ) ;
#2972=LINE ( 'NONE', #10291, #4628 ) ;
#2977=DIRECTION ( 'NONE',  ( 0.000000000000000000, 0.000000000000000000, 1.000000000000000000 ) ) ;
#2978=AXIS2_PLACEMENT_3D ( 'NONE', #969, #7491, #2508 ) ;
#2982=VECTOR ( 'NONE', #1093, 1000.000000000000000 ) ;
#2984=CARTESIAN_POINT ( 'NONE',  ( 17.58618750323380908, 6.000000000000000000, 0.000000000000000000 ) ) ;
#2987=ORIENTED_EDGE ( 'NONE', *, *, #8007, .T. ) ;
#2994=DIRECTION ( 'NONE',  ( 0.3420201433256627732, -0.9396926207859105373, 0.000000000000000000 ) ) ;
#2996=EDGE_CURVE ( 'NONE', #3003, #8333, #6156, .T. ) ;
#3000=ORIENTED_EDGE ( 'NONE', *, *, #8763, .T. ) ;
#3003=VERTEX_POINT ( 'NONE', #9408 ) ;
#3006=EDGE_LOOP ( 'NONE', ( #3032, #421, #7028, #8367 ) ) ;
#3009=ORIENTED_EDGE ( 'NONE', *, *, #5502, .T. ) ;
#3014=ORIENTED_EDGE ( 'NONE', *, *, #9849, .F. ) ;
#3023=DIRECTION ( 'NONE',  ( 0.000000000000000000, -1.000000000000000000, 0.000000000000000000 ) ) ;
#3026=FACE_OUTER_BOUND ( 'NONE', #355, .T. ) ;
#3032=ORIENTED_EDGE ( 'NONE', *, *, #5450, .F. ) ;
#3035=DIRECTION ( 'NONE',  ( -0.000000000000000000, -0.000000000000000000, 1.000000000000000000 ) ) ;
#3036=VECTOR ( 'NONE', #5680, 1000.000000000000000 ) ;
#3038=VECTOR ( 'NONE', #6715, 1000.000000000000000 ) ;
#3041=ORIENTED_EDGE ( 'NONE', *, *, #6947, .F. ) ;
#3045=AXIS2_PLACEMENT_3D ( 'NONE', #9437, #9271, #8531 ) ;
#3053=ORIENTED_EDGE ( 'NONE', *, *, #1059, .F. ) ;
#3054=EDGE_CURVE ( 'NONE', #4330, #2931, #4565, .T. ) ;
#3057=CARTESIAN_POINT ( 'NONE',  ( 1.272613240716556016, -10.02539999999999942, 0.000000000000000000 ) ) ;
#3070=DIRECTION ( 'NONE',  ( 0.000000000000000000, -0.000000000000000000, 1.000000000000000000 ) ) ;
#3074=LINE ( 'NONE', #8590, #2604 ) ;
#3075=EDGE_LOOP ( 'NONE', ( #3776, #3849, #1670, #7828 ) ) ;
#3077=FACE_OUTER_BOUND ( 'NONE', #4805, .T. ) ;
#3079=EDGE_CURVE ( 'NONE', #3593, #4169, #5156, .T. ) ;
#3080=DIRECTION ( 'NONE',  ( 0.000000000000000000, 1.000000000000000000, 0.000000000000000000 ) ) ;
#3086=ORIENTED_EDGE ( 'NONE', *, *, #7400, .F. ) ;
#3088=LINE ( 'NONE', #4669, #5327 ) ;
#3089=LINE ( 'NONE', #8706, #2982 ) ;
#3091=CARTESIAN_POINT ( 'NONE',  ( 0.000000000000000000, 6.000000000000000000, -12.00000000000000000 ) ) ;
#3092=DIRECTION ( 'NONE',  ( 0.3420201433256627732, 0.9396926207859105373, -0.000000000000000000 ) ) ;
#3100=ORIENTED_EDGE ( 'NONE', *, *, #3333, .T. ) ;
#3101=EDGE_CURVE ( 'NONE', #10205, #8915, #5315, .T. ) ;
#3102=EDGE_LOOP ( 'NONE', ( #6920, #6805, #831, #7243 ) ) ;
#3111=VERTEX_POINT ( 'NONE', #10000 ) ;
#3120=VECTOR ( 'NONE', #6352, 1000.000000000000000 ) ;
#3121=ORIENTED_EDGE ( 'NONE', *, *, #10406, .T. ) ;
#3127=EDGE_LOOP ( 'NONE', ( #5434, #156, #2381, #3839 ) ) ;
#3130=PLANE ( 'NONE',  #1343 ) ;
#3131=PLANE ( 'NONE',  #7897 ) ;
#3132=DIRECTION ( 'NONE',  ( 0.000000000000000000, 0.000000000000000000, 1.000000000000000000 ) ) ;
#3136=EDGE_CURVE ( 'NONE', #5844, #1096, #9248, .T. ) ;
#3137=DIRECTION ( 'NONE',  ( 0.3420201433256627732, -0.9396926207859105373, 0.000000000000000000 ) ) ;
#3144=CARTESIAN_POINT ( 'NONE',  ( 0.000000000000000000, -4.000000000000000000, -2.000000000000000000 ) ) ;
#3146=LINE ( 'NONE', #814, #8969 ) ;
#3147=VECTOR ( 'NONE', #406, 1000.000000000000000 ) ;
#3149=CARTESIAN_POINT ( 'NONE',  ( 25.00000000000000000, 0.000000000000000000, -12.00000000000000000 ) ) ;
#3150=VECTOR ( 'NONE', #1933, 1000.000000000000000 ) ;
#3158=ORIENTED_EDGE ( 'NONE', *, *, #5322, .F. ) ;
#3159=DIRECTION ( 'NONE',  ( 0.3420201433256627732, 0.9396926207859105373, 0.000000000000000000 ) ) ;
#3160=DIRECTION ( 'NONE',  ( 1.000000000000000000, 0.000000000000000000, 0.000000000000000000 ) ) ;
#3167=DIRECTION ( 'NONE',  ( 0.3420201433256627732, 0.9396926207859105373, 0.000000000000000000 ) ) ;
#3178=ORIENTED_EDGE ( 'NONE', *, *, #3101, .F. ) ;
#3180=CARTESIAN_POINT ( 'NONE',  ( 18.40512053033274853, 3.750000000000000000, -12.00000000000000000 ) ) ;
#3183=DIRECTION ( 'NONE',  ( 0.000000000000000000, -1.000000000000000000, -0.000000000000000000 ) ) ;
#3184=PLANE ( 'NONE',  #155 ) ;
#3186=ADVANCED_FACE ( 'NONE', ( #6372 ), #4786, .F. ) ;
#3187=VERTEX_POINT ( 'NONE', #8708 ) ;
#3192=ORIENTED_EDGE ( 'NONE', *, *, #2129, .T. ) ;
#3193=DIRECTION ( 'NONE',  ( 0.3420201433256627732, 0.9396926207859105373, -0.000000000000000000 ) ) ;
#3195=ORIENTED_EDGE ( 'NONE', *, *, #796, .T. ) ;
#3201=LINE ( 'NONE', #3149, #6256 ) ;
#3207=ORIENTED_EDGE ( 'NONE', *, *, #9955, .F. ) ;
#3209=ORIENTED_EDGE ( 'NONE', *, *, #5251, .T. ) ;
#3217=CARTESIAN_POINT ( 'NONE',  ( 13.83898384071655840, -10.02539999999999942, -12.00000000000000000 ) ) ;
#3220=ORIENTED_EDGE ( 'NONE', *, *, #9614, .F. ) ;
#3224=ORIENTED_EDGE ( 'NONE', *, *, #1292, .F. ) ;
#3227=EDGE_CURVE ( 'NONE', #6924, #1894, #1503, .T. ) ;
#3228=VECTOR ( 'NONE', #2942, 1000.000000000000000 ) ;
#3232=PLANE ( 'NONE',  #7189 ) ;
#3233=VECTOR ( 'NONE', #9792, 1000.000000000000000 ) ;
#3235=CARTESIAN_POINT ( 'NONE',  ( 14.44459485323380576, -10.00000000000000000, 0.000000000000000000 ) ) ;
#3238=VECTOR ( 'NONE', #4691, 1000.000000000000000 ) ;
#3241=VERTEX_POINT ( 'NONE', #6419 ) ;
#3243=VECTOR ( 'NONE', #929, 1000.000000000000000 ) ;
#3247=LINE ( 'NONE', #2297, #7869 ) ;
#3251=FACE_OUTER_BOUND ( 'NONE', #2470, .T. ) ;
#3252=DIRECTION ( 'NONE',  ( -1.000000000000000000, 0.000000000000000000, -0.000000000000000000 ) ) ;
#3253=DIRECTION ( 'NONE',  ( -1.000000000000000000, -0.000000000000000000, -0.000000000000000000 ) ) ;
#3258=ORIENTED_EDGE ( 'NONE', *, *, #3755, .F. ) ;
#3259=ADVANCED_FACE ( 'NONE', ( #3830 ), #10480, .F. ) ;
#3261=EDGE_CURVE ( 'NONE', #1356, #9713, #10422, .T. ) ;
#3268=EDGE_LOOP ( 'NONE', ( #2202, #3538, #9592, #3952 ) ) ;
#3275=PLANE ( 'NONE',  #10262 ) ;
#3279=LINE ( 'NONE', #2273, #417 ) ;
#3284=ORIENTED_EDGE ( 'NONE', *, *, #7190, .T. ) ;
#3299=FACE_OUTER_BOUND ( 'NONE', #3770, .T. ) ;
#3302=DIRECTION ( 'NONE',  ( 0.3420201433256627732, 0.9396926207859105373, 0.000000000000000000 ) ) ;
#3311=ORIENTED_EDGE ( 'NONE', *, *, #7459, .T. ) ;
#3312=CARTESIAN_POINT ( 'NONE',  ( 20.11292429676619520, -10.00000000000000000, 0.000000000000000000 ) ) ;
#3313=VECTOR ( 'NONE', #7916, 1000.000000000000000 ) ;
#3316=AXIS2_PLACEMENT_3D ( 'NONE', #5469, #1611, #6207 ) ;
#3320=ADVANCED_FACE ( 'NONE', ( #6259 ), #547, .F. ) ;
#3324=VERTEX_POINT ( 'NONE', #3144 ) ;
#3328=EDGE_LOOP ( 'NONE', ( #5899, #9960, #1043, #5486, #5114, #9946, #3009, #2531, #7366, #9869, #3753, #266, #1301, #8204, #5393, #4645, #8414, #7177, #995, #2271, #8736, #9385, #5336, #625, #2312, #1571, #3000, #7896, #4650, #7933, #8814, #7473, #10452, #5542, #3195, #186 ) ) ;
#3333=EDGE_CURVE ( 'NONE', #2958, #3937, #7918, .T. ) ;
#3335=VERTEX_POINT ( 'NONE', #6576 ) ;
#3336=CARTESIAN_POINT ( 'NONE',  ( 0.000000000000000000, 6.000000000000000000, -12.00000000000000000 ) ) ;
#3343=CARTESIAN_POINT ( 'NONE',  ( 22.43558391966725907, -7.750000000000000000, -12.00000000000000000 ) ) ;
#3354=CARTESIAN_POINT ( 'NONE',  ( 13.82973899676619745, 6.000000000000000000, -12.00000000000000000 ) ) ;
#3360=ORIENTED_EDGE ( 'NONE', *, *, #203, .F. ) ;
#3368=VECTOR ( 'NONE', #3159, 1000.000000000000000 ) ;
#3378=VERTEX_POINT ( 'NONE', #7275 ) ;
#3386=VECTOR ( 'NONE', #5592, 1000.000000000000000 ) ;
#3388=ADVANCED_FACE ( 'NONE', ( #5676 ), #5831, .T. ) ;
#3390=CARTESIAN_POINT ( 'NONE',  ( 1.878224253233805818, -10.00000000000000000, 0.000000000000000000 ) ) ;
#3391=FACE_OUTER_BOUND ( 'NONE', #3102, .T. ) ;
#3392=VERTEX_POINT ( 'NONE', #4195 ) ;
#3397=ORIENTED_EDGE ( 'NONE', *, *, #4198, .F. ) ;
#3398=VECTOR ( 'NONE', #10102, 1000.000000000000000 ) ;
#3399=DIRECTION ( 'NONE',  ( 0.000000000000000000, -1.000000000000000000, 0.000000000000000000 ) ) ;
#3400=EDGE_CURVE ( 'NONE', #3392, #10377, #7329, .T. ) ;
#3404=AXIS2_PLACEMENT_3D ( 'NONE', #599, #5364, #649 ) ;
#3423=ORIENTED_EDGE ( 'NONE', *, *, #4279, .T. ) ;
#3426=ADVANCED_FACE ( 'NONE', ( #3299 ), #9780, .T. ) ;
#3428=ORIENTED_EDGE ( 'NONE', *, *, #1991, .T. ) ;
#3429=DIRECTION ( 'NONE',  ( 0.000000000000000000, -1.000000000000000000, 0.000000000000000000 ) ) ;
#3431=ORIENTED_EDGE ( 'NONE', *, *, #874, .F. ) ;
#3435=ORIENTED_EDGE ( 'NONE', *, *, #925, .T. ) ;
#3446=VECTOR ( 'NONE', #8797, 1000.000000000000000 ) ;
#3459=LINE ( 'NONE', #6682, #10425 ) ;
#3463=EDGE_CURVE ( 'NONE', #3378, #5694, #8082, .T. ) ;
#3476=LINE ( 'NONE', #4212, #3950 ) ;
#3477=VERTEX_POINT ( 'NONE', #4042 ) ;
#3492=( NAMED_UNIT ( * ) PLANE_ANGLE_UNIT ( ) SI_UNIT ( $, .RADIAN. ) );
#3502=CARTESIAN_POINT ( 'NONE',  ( 13.01080596966725622, 3.750000000000000000, -12.00000000000000000 ) ) ;
#3503=CARTESIAN_POINT ( 'NONE',  ( 8.152164709283445276, -10.02539999999999942, -12.00000000000000000 ) ) ;
#3508=FACE_OUTER_BOUND ( 'NONE', #10119, .T. ) ;
#3517=EDGE_CURVE ( 'NONE', #5332, #4686, #3710, .T. ) ;
#3519=CARTESIAN_POINT ( 'NONE',  ( 9.869213319667256457, -7.750000000000000000, -12.00000000000000000 ) ) ;
#3520=ORIENTED_EDGE ( 'NONE', *, *, #6284, .F. ) ;
#3524=ORIENTED_EDGE ( 'NONE', *, *, #4095, .F. ) ;
#3527=ADVANCED_FACE ( 'NONE', ( #9344 ), #10197, .T. ) ;
#3529=LINE ( 'NONE', #9756, #2711 ) ;
#3538=ORIENTED_EDGE ( 'NONE', *, *, #10211, .T. ) ;
#3542=VERTEX_POINT ( 'NONE', #7699 ) ;
#3552=VECTOR ( 'NONE', #2315, 1000.000000000000000 ) ;
#3555=EDGE_CURVE ( 'NONE', #1356, #3874, #6890, .T. ) ;
#3559=DIRECTION ( 'NONE',  ( 0.000000000000000000, 0.000000000000000000, 1.000000000000000000 ) ) ;
#3569=VECTOR ( 'NONE', #37, 1000.000000000000000 ) ;
#3571=VECTOR ( 'NONE', #917, 1000.000000000000000 ) ;
#3579=ADVANCED_FACE ( 'NONE', ( #5253 ), #1923, .T. ) ;
#3582=VERTEX_POINT ( 'NONE', #2865 ) ;
#3583=DIRECTION ( 'NONE',  ( 0.000000000000000000, 1.000000000000000000, 0.000000000000000000 ) ) ;
#3584=CARTESIAN_POINT ( 'NONE',  ( 14.44459485323380754, 6.000000000000000000, -12.00000000000000000 ) ) ;
#3585=EDGE_LOOP ( 'NONE', ( #6436, #7529, #2698, #2800 ) ) ;
#3593=VERTEX_POINT ( 'NONE', #2078 ) ;
#3596=ORIENTED_EDGE ( 'NONE', *, *, #81, .F. ) ;
#3597=LINE ( 'NONE', #1858, #1175 ) ;
#3602=DIRECTION ( 'NONE',  ( 0.3420201433256627732, 0.9396926207859105373, 0.000000000000000000 ) ) ;
#3604=DIRECTION ( 'NONE',  ( 1.000000000000000000, 0.000000000000000000, 0.000000000000000000 ) ) ;
#3607=VECTOR ( 'NONE', #8248, 1000.000000000000000 ) ;
#3609=DIRECTION ( 'NONE',  ( 0.000000000000000000, 0.000000000000000000, -1.000000000000000000 ) ) ;
#3610=DIRECTION ( 'NONE',  ( -1.000000000000000000, 0.000000000000000000, -0.000000000000000000 ) ) ;
#3619=DIRECTION ( 'NONE',  ( 0.000000000000000000, 0.000000000000000000, -1.000000000000000000 ) ) ;
#3620=ORIENTED_EDGE ( 'NONE', *, *, #1292, .T. ) ;
#3633=LINE ( 'NONE', #1352, #684 ) ;
#3637=ADVANCED_FACE ( 'NONE', ( #3508 ), #1279, .F. ) ;
#3645=ORIENTED_EDGE ( 'NONE', *, *, #2088, .T. ) ;
#3646=LINE ( 'NONE', #469, #6168 ) ;
#3647=DIRECTION ( 'NONE',  ( 0.000000000000000000, -1.000000000000000000, -0.000000000000000000 ) ) ;
#3650=DIRECTION ( 'NONE',  ( -1.000000000000000000, -0.000000000000000000, -0.000000000000000000 ) ) ;
#3656=AXIS2_PLACEMENT_3D ( 'NONE', #2350, #6311, #10369 ) ;
#3657=CARTESIAN_POINT ( 'NONE',  ( 16.15239861966725599, -7.750000000000000000, 0.000000000000000000 ) ) ;
#3661=LINE ( 'NONE', #6835, #7719 ) ;
#3667=DIRECTION ( 'NONE',  ( -0.9396926207859105373, 0.3420201433256627732, 0.000000000000000000 ) ) ;
#3668=ORIENTED_EDGE ( 'NONE', *, *, #8731, .F. ) ;
#3672=DIRECTION ( 'NONE',  ( -1.000000000000000000, 0.000000000000000000, -0.000000000000000000 ) ) ;
#3673=EDGE_LOOP ( 'NONE', ( #8525, #6650, #8721, #4202 ) ) ;
#3681=ADVANCED_FACE ( 'NONE', ( #1226 ), #9394, .F. ) ;
#3686=ORIENTED_EDGE ( 'NONE', *, *, #2759, .T. ) ;
#3694=LINE ( 'NONE', #5385, #2968 ) ;
#3697=CARTESIAN_POINT ( 'NONE',  ( 0.4444353696672553311, 3.750000000000000000, -12.00000000000000000 ) ) ;
#3702=VECTOR ( 'NONE', #7850, 1000.000000000000000 ) ;
#3703=LINE ( 'NONE', #4500, #6300 ) ;
#3704=EDGE_CURVE ( 'NONE', #247, #7195, #1548, .T. ) ;
#3707=DIRECTION ( 'NONE',  ( 0.000000000000000000, 0.000000000000000000, 1.000000000000000000 ) ) ;
#3708=CARTESIAN_POINT ( 'NONE',  ( 8.152164709283445276, 6.025400000000000311, -12.00000000000000000 ) ) ;
#3709=DIRECTION ( 'NONE',  ( 0.000000000000000000, 0.000000000000000000, -1.000000000000000000 ) ) ;
#3710=LINE ( 'NONE', #436, #8732 ) ;
#3711=CARTESIAN_POINT ( 'NONE',  ( 25.00000000000000000, 0.000000000000000000, -12.00000000000000000 ) ) ;
#3719=ORIENTED_EDGE ( 'NONE', *, *, #7077, .T. ) ;
#3721=LINE ( 'NONE', #545, #858 ) ;
#3723=CARTESIAN_POINT ( 'NONE',  ( 1.263368396766194390, -10.00000000000000000, -12.00000000000000000 ) ) ;
#3731=ORIENTED_EDGE ( 'NONE', *, *, #1059, .T. ) ;
#3733=ORIENTED_EDGE ( 'NONE', *, *, #287, .T. ) ;
#3736=VECTOR ( 'NONE', #3773, 1000.000000000000000 ) ;
#3738=ORIENTED_EDGE ( 'NONE', *, *, #5254, .F. ) ;
#3748=PLANE ( 'NONE',  #3045 ) ;
#3750=CARTESIAN_POINT ( 'NONE',  ( 0.000000000000000000, 6.000000000000000000, 0.000000000000000000 ) ) ;
#3753=ORIENTED_EDGE ( 'NONE', *, *, #6802, .T. ) ;
#3754=DIRECTION ( 'NONE',  ( -1.000000000000000000, 0.000000000000000000, -0.000000000000000000 ) ) ;
#3755=EDGE_CURVE ( 'NONE', #5890, #4690, #4554, .T. ) ;
#3757=CARTESIAN_POINT ( 'NONE',  ( 25.00000000000000000, 0.000000000000000000, -10.00000000000000000 ) ) ;
#3758=DIRECTION ( 'NONE',  ( -0.000000000000000000, -0.000000000000000000, 1.000000000000000000 ) ) ;
#3759=PLANE ( 'NONE',  #4067 ) ;
#3761=CARTESIAN_POINT ( 'NONE',  ( 1.263368396766194390, 6.000000000000000000, -12.00000000000000000 ) ) ;
#3762=ADVANCED_FACE ( 'NONE', ( #2236 ), #3131, .T. ) ;
#3770=EDGE_LOOP ( 'NONE', ( #4414, #760, #10316, #4006, #3428, #609, #3620, #3520, #8615, #976, #2408, #6658 ) ) ;
#3772=DIRECTION ( 'NONE',  ( 0.000000000000000000, 0.000000000000000000, 1.000000000000000000 ) ) ;
#3773=DIRECTION ( 'NONE',  ( 0.000000000000000000, 0.000000000000000000, 1.000000000000000000 ) ) ;
#3776=ORIENTED_EDGE ( 'NONE', *, *, #10254, .F. ) ;
#3779=VECTOR ( 'NONE', #809, 1000.000000000000000 ) ;
#3780=DIRECTION ( 'NONE',  ( 0.000000000000000000, 0.000000000000000000, 1.000000000000000000 ) ) ;
#3783=ORIENTED_EDGE ( 'NONE', *, *, #4350, .T. ) ;
#3788=VERTEX_POINT ( 'NONE', #7212 ) ;
#3790=ORIENTED_EDGE ( 'NONE', *, *, #1580, .F. ) ;
#3791=LINE ( 'NONE', #9431, #4085 ) ;
#3797=VERTEX_POINT ( 'NONE', #9657 ) ;
#3798=CARTESIAN_POINT ( 'NONE',  ( 9.869213319667256457, 3.750000000000000000, 0.000000000000000000 ) ) ;
#3799=EDGE_CURVE ( 'NONE', #6026, #7306, #10410, .T. ) ;
#3805=AXIS2_PLACEMENT_3D ( 'NONE', #1738, #9207, #10116 ) ;
#3807=CARTESIAN_POINT ( 'NONE',  ( 11.30300220323380600, -10.00000000000000000, -12.00000000000000000 ) ) ;
#3809=CARTESIAN_POINT ( 'NONE',  ( 0.000000000000000000, 0.000000000000000000, -12.00000000000000000 ) ) ;
#3811=AXIS2_PLACEMENT_3D ( 'NONE', #9779, #2507, #4784 ) ;
#3823=AXIS2_PLACEMENT_3D ( 'NONE', #9559, #3183, #9450 ) ;
#3824=VERTEX_POINT ( 'NONE', #3980 ) ;
#3827=CARTESIAN_POINT ( 'NONE',  ( 16.15239861966725599, 3.750000000000000000, -12.00000000000000000 ) ) ;
#3830=FACE_OUTER_BOUND ( 'NONE', #3900, .T. ) ;
#3832=ORIENTED_EDGE ( 'NONE', *, *, #5450, .T. ) ;
#3833=CARTESIAN_POINT ( 'NONE',  ( 4.414205890716556446, 6.025400000000000311, 0.000000000000000000 ) ) ;
#3838=EDGE_CURVE ( 'NONE', #8274, #3582, #4771, .T. ) ;
#3839=ORIENTED_EDGE ( 'NONE', *, *, #4881, .F. ) ;
#3841=CARTESIAN_POINT ( 'NONE',  ( 7.206705994753384914, -12.62302646919798299, 0.000000000000000000 ) ) ;
#3849=ORIENTED_EDGE ( 'NONE', *, *, #9352, .F. ) ;
#3852=ORIENTED_EDGE ( 'NONE', *, *, #5378, .F. ) ;
#3854=CARTESIAN_POINT ( 'NONE',  ( 13.82973899676619745, 6.000000000000000000, 0.000000000000000000 ) ) ;
#3866=DIRECTION ( 'NONE',  ( 1.000000000000000000, -0.000000000000000000, -0.000000000000000000 ) ) ;
#3874=VERTEX_POINT ( 'NONE', #4083 ) ;
#3875=LINE ( 'NONE', #8921, #10252 ) ;
#3880=DIRECTION ( 'NONE',  ( 1.000000000000000000, 0.000000000000000000, 0.000000000000000000 ) ) ;
#3882=ORIENTED_EDGE ( 'NONE', *, *, #2076, .F. ) ;
#3885=LINE ( 'NONE', #5577, #9497 ) ;
#3886=VECTOR ( 'NONE', #6358, 1000.000000000000000 ) ;
#3900=EDGE_LOOP ( 'NONE', ( #1885, #5823, #577, #8209 ) ) ;
#3902=EDGE_CURVE ( 'NONE', #4597, #2608, #8857, .T. ) ;
#3919=LINE ( 'NONE', #5503, #3446 ) ;
#3924=DIRECTION ( 'NONE',  ( -0.9396926207859105373, -0.3420201433256627732, 0.000000000000000000 ) ) ;
#3927=DIRECTION ( 'NONE',  ( 1.000000000000000000, 0.000000000000000000, 0.000000000000000000 ) ) ;
#3931=PRODUCT_DEFINITION ( 'UNKNOWN', '', #6341, #5228 ) ;
#3932=CARTESIAN_POINT ( 'NONE',  ( 0.000000000000000000, 6.000000000000000000, 0.000000000000000000 ) ) ;
#3935=LINE ( 'NONE', #7328, #10445 ) ;
#3937=VERTEX_POINT ( 'NONE', #9770 ) ;
#3939=DIRECTION ( 'NONE',  ( 1.000000000000000000, -0.000000000000000000, -0.000000000000000000 ) ) ;
#3950=VECTOR ( 'NONE', #9150, 1000.000000000000000 ) ;
#3951=DIRECTION ( 'NONE',  ( 0.3420201433256627732, -0.9396926207859105373, 0.000000000000000000 ) ) ;
#3952=ORIENTED_EDGE ( 'NONE', *, *, #5738, .F. ) ;
#3954=LINE ( 'NONE', #2425, #1345 ) ;
#3955=ORIENTED_EDGE ( 'NONE', *, *, #9419, .T. ) ;
#3963=CARTESIAN_POINT ( 'NONE',  ( 20.72778015323380529, 6.000000000000000000, -12.00000000000000000 ) ) ;
#3975=ORIENTED_EDGE ( 'NONE', *, *, #414, .F. ) ;
#3980=CARTESIAN_POINT ( 'NONE',  ( 0.000000000000000000, -7.750000000000000000, 0.000000000000000000 ) ) ;
#3985=ORIENTED_EDGE ( 'NONE', *, *, #3261, .F. ) ;
#3986=LINE ( 'NONE', #7217, #10179 ) ;
#3990=ORIENTED_EDGE ( 'NONE', *, *, #8095, .F. ) ;
#4006=ORIENTED_EDGE ( 'NONE', *, *, #2129, .F. ) ;
#4009=ADVANCED_FACE ( 'NONE', ( #9818 ), #9073, .F. ) ;
#4015=ORIENTED_EDGE ( 'NONE', *, *, #9970, .F. ) ;
#4021=DIRECTION ( 'NONE',  ( 0.3420201433256627732, -0.9396926207859105373, 0.000000000000000000 ) ) ;
#4023=ORIENTED_EDGE ( 'NONE', *, *, #1815, .T. ) ;
#4031=FACE_OUTER_BOUND ( 'NONE', #9142, .T. ) ;
#4034=CARTESIAN_POINT ( 'NONE',  ( 5.838749930332745919, -7.750000000000000000, -12.00000000000000000 ) ) ;
#4035=ADVANCED_FACE ( 'NONE', ( #8226 ), #4185, .F. ) ;
#4042=CARTESIAN_POINT ( 'NONE',  ( 18.40512053033274853, -7.750000000000000000, 0.000000000000000000 ) ) ;
#4043=CARTESIAN_POINT ( 'NONE',  ( 23.26376179071655770, 6.025400000000000311, -12.00000000000000000 ) ) ;
#4054=EDGE_LOOP ( 'NONE', ( #1910, #8994, #3258, #1361 ) ) ;
#4058=ORIENTED_EDGE ( 'NONE', *, *, #1767, .F. ) ;
#4060=EDGE_CURVE ( 'NONE', #5694, #9178, #8533, .T. ) ;
#4064=( GEOMETRIC_REPRESENTATION_CONTEXT ( 3 ) GLOBAL_UNCERTAINTY_ASSIGNED_CONTEXT ( ( #1569 ) ) GLOBAL_UNIT_ASSIGNED_CONTEXT ( ( #5698, #8265, #255 ) ) REPRESENTATION_CONTEXT ( 'NONE', 'WORKASPACE' ) );
#4067=AXIS2_PLACEMENT_3D ( 'NONE', #634, #3023, #694 ) ;
#4076=VECTOR ( 'NONE', #7054, 1000.000000000000000 ) ;
#4080=AXIS2_PLACEMENT_3D ( 'NONE', #5316, #7760, #7599 ) ;
#4083=CARTESIAN_POINT ( 'NONE',  ( 5.838749930332745919, -7.750000000000000000, 0.000000000000000000 ) ) ;
#4085=VECTOR ( 'NONE', #10173, 1000.000000000000000 ) ;
#4094=CARTESIAN_POINT ( 'NONE',  ( 4.414205890716556446, 6.025400000000000311, -12.00000000000000000 ) ) ;
#4095=EDGE_CURVE ( 'NONE', #138, #6440, #6823, .T. ) ;
#4097=EDGE_CURVE ( 'NONE', #9757, #1996, #3597, .T. ) ;
#4099=LINE ( 'NONE', #6374, #5736 ) ;
#4114=ORIENTED_EDGE ( 'NONE', *, *, #1991, .F. ) ;
#4116=AXIS2_PLACEMENT_3D ( 'NONE', #7220, #9456, #8654 ) ;
#4118=SURFACE_STYLE_USAGE ( .BOTH. , #1739 ) ;
#4132=CARTESIAN_POINT ( 'NONE',  ( 25.57717656966725883, 3.750000000000000000, -12.00000000000000000 ) ) ;
#4143=CARTESIAN_POINT ( 'NONE',  ( 0.000000000000000000, 6.000000000000000000, 0.000000000000000000 ) ) ;
#4146=DIRECTION ( 'NONE',  ( 0.3420201433256627732, 0.9396926207859105373, 0.000000000000000000 ) ) ;
#4155=EDGE_LOOP ( 'NONE', ( #5918, #8662, #7720, #10432 ) ) ;
#4158=AXIS2_PLACEMENT_3D ( 'NONE', #124, #2298, #5522 ) ;
#4159=CARTESIAN_POINT ( 'NONE',  ( 13.01080596966725622, 3.750000000000000000, -12.00000000000000000 ) ) ;
#4161=VECTOR ( 'NONE', #6144, 1000.000000000000000 ) ;
#4165=EDGE_CURVE ( 'NONE', #2377, #7824, #5081, .T. ) ;
#4168=VECTOR ( 'NONE', #7319, 1000.000000000000000 ) ;
#4169=VERTEX_POINT ( 'NONE', #6669 ) ;
#4178=EDGE_CURVE ( 'NONE', #6828, #9702, #5968, .T. ) ;
#4180=ORIENTED_EDGE ( 'NONE', *, *, #5783, .T. ) ;
#4181=DIRECTION ( 'NONE',  ( 0.9396926207859105373, 0.3420201433256627732, 0.000000000000000000 ) ) ;
#4182=CARTESIAN_POINT ( 'NONE',  ( 23.86012795928344588, 6.025400000000000311, -12.00000000000000000 ) ) ;
#4185=PLANE ( 'NONE',  #333 ) ;
#4189=FACE_OUTER_BOUND ( 'NONE', #7953, .T. ) ;
#4192=DIRECTION ( 'NONE',  ( 0.000000000000000000, 0.000000000000000000, 1.000000000000000000 ) ) ;
#4195=CARTESIAN_POINT ( 'NONE',  ( 14.44459485323380576, -10.00000000000000000, -12.00000000000000000 ) ) ;
#4198=EDGE_CURVE ( 'NONE', #1471, #6291, #7526, .T. ) ;
#4201=LINE ( 'NONE', #9136, #8193 ) ;
#4202=ORIENTED_EDGE ( 'NONE', *, *, #5192, .T. ) ;
#4209=ORIENTED_EDGE ( 'NONE', *, *, #1158, .T. ) ;
#4212=CARTESIAN_POINT ( 'NONE',  ( 3.586028019667255595, 3.750000000000000000, -12.00000000000000000 ) ) ;
#4215=VERTEX_POINT ( 'NONE', #1266 ) ;
#4219=ORIENTED_EDGE ( 'NONE', *, *, #8738, .T. ) ;
#4239=LINE ( 'NONE', #8283, #2886 ) ;
#4252=VERTEX_POINT ( 'NONE', #4697 ) ;
#4254=EDGE_CURVE ( 'NONE', #4487, #6626, #521, .T. ) ;
#4257=ORIENTED_EDGE ( 'NONE', *, *, #3136, .F. ) ;
#4267=LINE ( 'NONE', #8943, #6851 ) ;
#4268=SURFACE_STYLE_FILL_AREA ( #9002 ) ;
#4277=EDGE_CURVE ( 'NONE', #4895, #7351, #6232, .T. ) ;
#4278=( NAMED_UNIT ( * ) SI_UNIT ( $, .STERADIAN. ) SOLID_ANGLE_UNIT ( ) );
#4279=EDGE_CURVE ( 'NONE', #1347, #4726, #1420, .T. ) ;
#4280=VERTEX_POINT ( 'NONE', #680 ) ;
#4282=FACE_OUTER_BOUND ( 'NONE', #311, .T. ) ;
#4289=CARTESIAN_POINT ( 'NONE',  ( 0.000000000000000000, -10.00000000000000000, -12.00000000000000000 ) ) ;
#4295=DIRECTION ( 'NONE',  ( 0.000000000000000000, 0.000000000000000000, 1.000000000000000000 ) ) ;
#4300=EDGE_CURVE ( 'NONE', #8225, #1785, #2272, .T. ) ;
#4302=ORIENTED_EDGE ( 'NONE', *, *, #9033, .F. ) ;
#4306=DIRECTION ( 'NONE',  ( -0.9396926207859105373, 0.3420201433256627732, 0.000000000000000000 ) ) ;
#4307=VERTEX_POINT ( 'NONE', #6925 ) ;
#4308=VECTOR ( 'NONE', #4434, 1000.000000000000000 ) ;
#4313=VERTEX_POINT ( 'NONE', #2167 ) ;
#4314=AXIS2_PLACEMENT_3D ( 'NONE', #1417, #8734, #10450 ) ;
#4315=VERTEX_POINT ( 'NONE', #5390 ) ;
#4328=VECTOR ( 'NONE', #3866, 1000.000000000000000 ) ;
#4329=( NAMED_UNIT ( * ) SI_UNIT ( $, .STERADIAN. ) SOLID_ANGLE_UNIT ( ) );
#4330=VERTEX_POINT ( 'NONE', #6184 ) ;
#4334=ORIENTED_EDGE ( 'NONE', *, *, #1635, .F. ) ;
#4336=DIRECTION ( 'NONE',  ( 0.000000000000000000, -1.000000000000000000, -0.000000000000000000 ) ) ;
#4345=DIRECTION ( 'NONE',  ( 0.000000000000000000, 0.000000000000000000, 1.000000000000000000 ) ) ;
#4350=EDGE_CURVE ( 'NONE', #946, #9203, #572, .T. ) ;
#4356=CARTESIAN_POINT ( 'NONE',  ( 3.586028019667255595, -7.750000000000000000, -12.00000000000000000 ) ) ;
#4361=LINE ( 'NONE', #5210, #7274 ) ;
#4364=ORIENTED_EDGE ( 'NONE', *, *, #2586, .T. ) ;
#4368=DIRECTION ( 'NONE',  ( 1.000000000000000000, -0.000000000000000000, -0.000000000000000000 ) ) ;
#4383=ORIENTED_EDGE ( 'NONE', *, *, #387, .T. ) ;
#4384=DIRECTION ( 'NONE',  ( 0.3420201433256627732, -0.9396926207859105373, 0.000000000000000000 ) ) ;
#4400=CARTESIAN_POINT ( 'NONE',  ( 16.15239861966725599, -7.750000000000000000, -12.00000000000000000 ) ) ;
#4407=VERTEX_POINT ( 'NONE', #7130 ) ;
#4410=EDGE_CURVE ( 'NONE', #9328, #3187, #5538, .T. ) ;
#4413=PLANE ( 'NONE',  #2559 ) ;
#4414=ORIENTED_EDGE ( 'NONE', *, *, #8007, .F. ) ;
#4424=DIRECTION ( 'NONE',  ( 0.000000000000000000, 1.000000000000000000, 0.000000000000000000 ) ) ;
#4426=VERTEX_POINT ( 'NONE', #10276 ) ;
#4434=DIRECTION ( 'NONE',  ( 0.3420201433256627732, -0.9396926207859105373, 0.000000000000000000 ) ) ;
#4437=ORIENTED_EDGE ( 'NONE', *, *, #9033, .T. ) ;
#4440=CARTESIAN_POINT ( 'NONE',  ( 25.00000000000000000, -4.000000000000000000, -2.000000000000000000 ) ) ;
#4442=VERTEX_POINT ( 'NONE', #6120 ) ;
#4443=LINE ( 'NONE', #7692, #10191 ) ;
#4446=ADVANCED_FACE ( 'NONE', ( #6330 ), #1521, .T. ) ;
#4449=CARTESIAN_POINT ( 'NONE',  ( 11.29375735928344504, -10.02539999999999942, -12.00000000000000000 ) ) ;
#4450=EDGE_CURVE ( 'NONE', #4315, #8225, #507, .T. ) ;
#4451=DIRECTION ( 'NONE',  ( 0.000000000000000000, -1.000000000000000000, 0.000000000000000000 ) ) ;
#4460=CARTESIAN_POINT ( 'NONE',  ( 0.000000000000000000, 0.000000000000000000, 0.000000000000000000 ) ) ;
#4463=PLANE ( 'NONE',  #4080 ) ;
#4465=VECTOR ( 'NONE', #5655, 1000.000000000000000 ) ;
#4473=ORIENTED_EDGE ( 'NONE', *, *, #9019, .T. ) ;
#4482=ORIENTED_EDGE ( 'NONE', *, *, #996, .F. ) ;
#4487=VERTEX_POINT ( 'NONE', #7073 ) ;
#4493=VECTOR ( 'NONE', #4884, 1000.000000000000000 ) ;
#4494=LINE ( 'NONE', #574, #5818 ) ;
#4498=VECTOR ( 'NONE', #1819, 1000.000000000000000 ) ;
#4500=CARTESIAN_POINT ( 'NONE',  ( 0.000000000000000000, 6.000000000000000000, -12.00000000000000000 ) ) ;
#4515=EDGE_CURVE ( 'NONE', #1597, #6552, #9699, .T. ) ;
#4526=EDGE_CURVE ( 'NONE', #3111, #5332, #3954, .T. ) ;
#4527=PLANE ( 'NONE',  #6601 ) ;
#4537=EDGE_CURVE ( 'NONE', #244, #10205, #140, .T. ) ;
#4540=CARTESIAN_POINT ( 'NONE',  ( 13.82973899676619745, -10.00000000000000000, -12.00000000000000000 ) ) ;
#4541=FACE_OUTER_BOUND ( 'NONE', #10257, .T. ) ;
#4547=DIRECTION ( 'NONE',  ( 1.000000000000000000, 0.000000000000000000, 0.000000000000000000 ) ) ;
#4548=VECTOR ( 'NONE', #6769, 1000.000000000000000 ) ;
#4554=LINE ( 'NONE', #3761, #1975 ) ;
#4555=DIRECTION ( 'NONE',  ( 0.3420201433256627732, -0.9396926207859105373, 0.000000000000000000 ) ) ;
#4560=CARTESIAN_POINT ( 'NONE',  ( 17.57694265928344635, -10.02539999999999942, -12.00000000000000000 ) ) ;
#4561=ORIENTED_EDGE ( 'NONE', *, *, #5229, .F. ) ;
#4563=LINE ( 'NONE', #6152, #8816 ) ;
#4564=CARTESIAN_POINT ( 'NONE',  ( 0.000000000000000000, -10.00000000000000000, 0.000000000000000000 ) ) ;
#4565=LINE ( 'NONE', #8506, #3150 ) ;
#4566=LINE ( 'NONE', #5416, #5418 ) ;
#4570=CARTESIAN_POINT ( 'NONE',  ( 19.29399126966725575, -7.750000000000000000, -12.00000000000000000 ) ) ;
#4575=ORIENTED_EDGE ( 'NONE', *, *, #4867, .T. ) ;
#4578=ORIENTED_EDGE ( 'NONE', *, *, #9352, .T. ) ;
#4579=DIRECTION ( 'NONE',  ( 0.3420201433256627732, -0.9396926207859105373, 0.000000000000000000 ) ) ;
#4582=VERTEX_POINT ( 'NONE', #9640 ) ;
#4586=ORIENTED_EDGE ( 'NONE', *, *, #2218, .T. ) ;
#4588=EDGE_CURVE ( 'NONE', #5003, #4330, #7240, .T. ) ;
#4592=FACE_OUTER_BOUND ( 'NONE', #1994, .T. ) ;
#4597=VERTEX_POINT ( 'NONE', #5012 ) ;
#4599=EDGE_CURVE ( 'NONE', #5555, #6919, #4852, .T. ) ;
#4605=CARTESIAN_POINT ( 'NONE',  ( 13.01080596966725622, -7.750000000000000000, -12.00000000000000000 ) ) ;
#4606=PLANE ( 'NONE',  #1799 ) ;
#4608=CARTESIAN_POINT ( 'NONE',  ( 8.152164709283445276, -10.02539999999999942, -12.00000000000000000 ) ) ;
#4611=ADVANCED_FACE ( 'NONE', ( #41 ), #2478, .T. ) ;
#4613=FACE_OUTER_BOUND ( 'NONE', #7290, .T. ) ;
#4618=CARTESIAN_POINT ( 'NONE',  ( 8.980342580332745683, -7.750000000000000000, -12.00000000000000000 ) ) ;
#4626=ORIENTED_EDGE ( 'NONE', *, *, #7509, .F. ) ;
#4628=VECTOR ( 'NONE', #1378, 1000.000000000000000 ) ;
#4631=ORIENTED_EDGE ( 'NONE', *, *, #2671, .F. ) ;
#4635=ORIENTED_EDGE ( 'NONE', *, *, #985, .F. ) ;
#4636=DIRECTION ( 'NONE',  ( 0.000000000000000000, 1.000000000000000000, 0.000000000000000000 ) ) ;
#4639=ORIENTED_EDGE ( 'NONE', *, *, #8731, .T. ) ;
#4642=DIRECTION ( 'NONE',  ( 0.000000000000000000, -1.000000000000000000, 0.000000000000000000 ) ) ;
#4645=ORIENTED_EDGE ( 'NONE', *, *, #7937, .F. ) ;
#4647=EDGE_CURVE ( 'NONE', #2213, #6828, #4361, .T. ) ;
#4648=DIRECTION ( 'NONE',  ( 0.9396926207859105373, -0.3420201433256627732, 0.000000000000000000 ) ) ;
#4650=ORIENTED_EDGE ( 'NONE', *, *, #3463, .T. ) ;
#4652=DIRECTION ( 'NONE',  ( 1.000000000000000000, -0.000000000000000000, -0.000000000000000000 ) ) ;
#4655=CARTESIAN_POINT ( 'NONE',  ( 16.98057649071655817, 6.025400000000000311, -12.00000000000000000 ) ) ;
#4658=CARTESIAN_POINT ( 'NONE',  ( 19.29399126966725575, -7.750000000000000000, -12.00000000000000000 ) ) ;
#4667=ORIENTED_EDGE ( 'NONE', *, *, #567, .T. ) ;
#4669=CARTESIAN_POINT ( 'NONE',  ( 7.555798540716556211, -10.02539999999999942, 0.000000000000000000 ) ) ;
#4671=ADVANCED_FACE ( 'NONE', ( #1138 ), #9301, .T. ) ;
#4676=ORIENTED_EDGE ( 'NONE', *, *, #9166, .T. ) ;
#4677=CARTESIAN_POINT ( 'NONE',  ( 13.82973899676619745, 6.000000000000000000, -12.00000000000000000 ) ) ;
#4681=ORIENTED_EDGE ( 'NONE', *, *, #9432, .F. ) ;
#4686=VERTEX_POINT ( 'NONE', #5111 ) ;
#4688=LINE ( 'NONE', #2014, #3368 ) ;
#4690=VERTEX_POINT ( 'NONE', #7451 ) ;
#4691=DIRECTION ( 'NONE',  ( 0.000000000000000000, 0.000000000000000000, 1.000000000000000000 ) ) ;
#4694=CARTESIAN_POINT ( 'NONE',  ( 21.54671318033274829, 3.750000000000000000, 0.000000000000000000 ) ) ;
#4696=EDGE_LOOP ( 'NONE', ( #2945, #1526, #793, #3733 ) ) ;
#4697=CARTESIAN_POINT ( 'NONE',  ( 3.586028019667255595, 3.750000000000000000, 0.000000000000000000 ) ) ;
#4698=CARTESIAN_POINT ( 'NONE',  ( 0.4444353696672553311, 3.750000000000000000, 0.000000000000000000 ) ) ;
#4702=LINE ( 'NONE', #2123, #2094 ) ;
#4710=CARTESIAN_POINT ( 'NONE',  ( 18.40512053033274853, -7.750000000000000000, -12.00000000000000000 ) ) ;
#4726=VERTEX_POINT ( 'NONE', #9098 ) ;
#4727=CARTESIAN_POINT ( 'NONE',  ( 25.00000000000000000, -4.000000000000000000, -10.00000000000000000 ) ) ;
#4736=EDGE_CURVE ( 'NONE', #3797, #4252, #9200, .T. ) ;
#4744=VECTOR ( 'NONE', #2994, 1000.000000000000000 ) ;
#4745=PLANE ( 'NONE',  #5059 ) ;
#4753=ORIENTED_EDGE ( 'NONE', *, *, #1500, .F. ) ;
#4754=ORIENTED_EDGE ( 'NONE', *, *, #4178, .F. ) ;
#4755=VECTOR ( 'NONE', #1654, 1000.000000000000000 ) ;
#4762=CARTESIAN_POINT ( 'NONE',  ( 7.546553696766196140, -10.00000000000000000, -12.00000000000000000 ) ) ;
#4766=PLANE ( 'NONE',  #9377 ) ;
#4769=LINE ( 'NONE', #2600, #8823 ) ;
#4771=LINE ( 'NONE', #10466, #5178 ) ;
#4772=CARTESIAN_POINT ( 'NONE',  ( 22.43558391966725907, 3.750000000000000000, -12.00000000000000000 ) ) ;
#4779=PLANE ( 'NONE',  #1754 ) ;
#4784=DIRECTION ( 'NONE',  ( 0.000000000000000000, 0.000000000000000000, -1.000000000000000000 ) ) ;
#4786=PLANE ( 'NONE',  #3656 ) ;
#4787=CARTESIAN_POINT ( 'NONE',  ( 16.98057649071655817, 6.025400000000000311, -12.00000000000000000 ) ) ;
#4793=VECTOR ( 'NONE', #5497, 1000.000000000000000 ) ;
#4795=ORIENTED_EDGE ( 'NONE', *, *, #5697, .F. ) ;
#4800=VERTEX_POINT ( 'NONE', #5318 ) ;
#4802=EDGE_CURVE ( 'NONE', #7195, #4215, #6960, .T. ) ;
#4805=EDGE_LOOP ( 'NONE', ( #3311, #497, #6112, #7712 ) ) ;
#4806=VECTOR ( 'NONE', #6240, 1000.000000000000000 ) ;
#4810=EDGE_CURVE ( 'NONE', #4950, #1471, #10213, .T. ) ;
#4812=EDGE_CURVE ( 'NONE', #9748, #7999, #8510, .T. ) ;
#4813=CARTESIAN_POINT ( 'NONE',  ( 0.000000000000000000, 6.000000000000000000, -12.00000000000000000 ) ) ;
#4815=AXIS2_PLACEMENT_3D ( 'NONE', #7739, #4648, #6131 ) ;
#4816=ORIENTED_EDGE ( 'NONE', *, *, #414, .T. ) ;
#4818=( GEOMETRIC_REPRESENTATION_CONTEXT ( 3 ) GLOBAL_UNCERTAINTY_ASSIGNED_CONTEXT ( ( #7282 ) ) GLOBAL_UNIT_ASSIGNED_CONTEXT ( ( #1906, #3492, #4329 ) ) REPRESENTATION_CONTEXT ( 'NONE', 'WORKASPACE' ) );
#4820=LINE ( 'NONE', #6401, #7009 ) ;
#4822=CARTESIAN_POINT ( 'NONE',  ( 19.29399126966725575, -7.750000000000000000, 0.000000000000000000 ) ) ;
#4829=VECTOR ( 'NONE', #9560, 1000.000000000000000 ) ;
#4831=CARTESIAN_POINT ( 'NONE',  ( 16.15239861966725599, 3.750000000000000000, -12.00000000000000000 ) ) ;
#4833=DIRECTION ( 'NONE',  ( 1.000000000000000000, -0.000000000000000000, -0.000000000000000000 ) ) ;
#4834=AXIS2_PLACEMENT_3D ( 'NONE', #5415, #8660, #7165 ) ;
#4837=LINE ( 'NONE', #74, #9510 ) ;
#4846=ORIENTED_EDGE ( 'NONE', *, *, #8389, .F. ) ;
#4850=ORIENTED_EDGE ( 'NONE', *, *, #3799, .T. ) ;
#4852=LINE ( 'NONE', #2523, #2706 ) ;
#4857=EDGE_CURVE ( 'NONE', #4426, #2398, #9413, .T. ) ;
#4867=EDGE_CURVE ( 'NONE', #6026, #6209, #5368, .T. ) ;
#4871=PRODUCT_DEFINITION_SHAPE ( 'NONE', 'NONE',  #3931 ) ;
#4872=LINE ( 'NONE', #9815, #1946 ) ;
#4881=EDGE_CURVE ( 'NONE', #3335, #3788, #3885, .T. ) ;
#4884=DIRECTION ( 'NONE',  ( 0.3420201433256627732, 0.9396926207859105373, -0.000000000000000000 ) ) ;
#4888=VERTEX_POINT ( 'NONE', #7280 ) ;
#4895=VERTEX_POINT ( 'NONE', #2355 ) ;
#4901=ORIENTED_EDGE ( 'NONE', *, *, #6017, .F. ) ;
#4902=VECTOR ( 'NONE', #6621, 1000.000000000000000 ) ;
#4911=EDGE_CURVE ( 'NONE', #6440, #6214, #816, .T. ) ;
#4915=ORIENTED_EDGE ( 'NONE', *, *, #3838, .F. ) ;
#4935=ORIENTED_EDGE ( 'NONE', *, *, #3101, .T. ) ;
#4936=EDGE_CURVE ( 'NONE', #1004, #4313, #3201, .T. ) ;
#4943=PLANE ( 'NONE',  #365 ) ;
#4946=EDGE_CURVE ( 'NONE', #6306, #8274, #876, .T. ) ;
#4950=VERTEX_POINT ( 'NONE', #10427 ) ;
#4961=ORIENTED_EDGE ( 'NONE', *, *, #4526, .T. ) ;
#4964=CARTESIAN_POINT ( 'NONE',  ( 0.4444353696672553311, -7.750000000000000000, 0.000000000000000000 ) ) ;
#4967=ORIENTED_EDGE ( 'NONE', *, *, #3555, .F. ) ;
#4977=CARTESIAN_POINT ( 'NONE',  ( 4.404961046766194599, 6.000000000000000000, 0.000000000000000000 ) ) ;
#4978=DIRECTION ( 'NONE',  ( 0.3420201433256627732, 0.9396926207859105373, 0.000000000000000000 ) ) ;
#4979=VERTEX_POINT ( 'NONE', #78 ) ;
#4980=AXIS2_PLACEMENT_3D ( 'NONE', #8947, #2327, #9709 ) ;
#4988=VECTOR ( 'NONE', #5147, 1000.000000000000000 ) ;
#4989=LINE ( 'NONE', #965, #8877 ) ;
#4997=DIRECTION ( 'NONE',  ( -0.000000000000000000, -0.000000000000000000, 1.000000000000000000 ) ) ;
#5002=CARTESIAN_POINT ( 'NONE',  ( 0.000000000000000000, 0.000000000000000000, 0.000000000000000000 ) ) ;
#5003=VERTEX_POINT ( 'NONE', #8876 ) ;
#5008=VECTOR ( 'NONE', #1168, 1000.000000000000000 ) ;
#5011=CARTESIAN_POINT ( 'NONE',  ( 11.30300220323380600, -10.00000000000000000, 0.000000000000000000 ) ) ;
#5012=CARTESIAN_POINT ( 'NONE',  ( 24.68830583033274806, -7.750000000000000000, -12.00000000000000000 ) ) ;
#5013=ORIENTED_EDGE ( 'NONE', *, *, #5820, .T. ) ;
#5016=ORIENTED_EDGE ( 'NONE', *, *, #2759, .F. ) ;
#5019=ORIENTED_EDGE ( 'NONE', *, *, #7643, .F. ) ;
#5031=DIRECTION ( 'NONE',  ( 0.3420201433256627732, 0.9396926207859105373, 0.000000000000000000 ) ) ;
#5043=LINE ( 'NONE', #7647, #4988 ) ;
#5052=PLANE ( 'NONE',  #8326 ) ;
#5057=ADVANCED_FACE ( 'NONE', ( #2234 ), #3759, .T. ) ;
#5058=ADVANCED_FACE ( 'NONE', ( #3077 ), #6989, .F. ) ;
#5059=AXIS2_PLACEMENT_3D ( 'NONE', #4440, #7072, #6024 ) ;
#5071=ORIENTED_EDGE ( 'NONE', *, *, #5201, .F. ) ;
#5075=SURFACE_STYLE_USAGE ( .BOTH. , #5286 ) ;
#5080=ORIENTED_EDGE ( 'NONE', *, *, #1379, .T. ) ;
#5081=LINE ( 'NONE', #270, #6922 ) ;
#5082=VECTOR ( 'NONE', #2789, 1000.000000000000000 ) ;
#5086=VECTOR ( 'NONE', #1452, 1000.000000000000000 ) ;
#5087=CARTESIAN_POINT ( 'NONE',  ( 21.54671318033274829, -7.750000000000000000, -12.00000000000000000 ) ) ;
#5094=CARTESIAN_POINT ( 'NONE',  ( 7.555798540716556211, 6.025400000000000311, -12.00000000000000000 ) ) ;
#5095=CARTESIAN_POINT ( 'NONE',  ( 0.000000000000000000, -10.00000000000000000, -12.00000000000000000 ) ) ;
#5104=ORIENTED_EDGE ( 'NONE', *, *, #10254, .T. ) ;
#5107=EDGE_CURVE ( 'NONE', #3824, #9213, #7799, .T. ) ;
#5110=CARTESIAN_POINT ( 'NONE',  ( 0.000000000000000000, -10.00000000000000000, -12.00000000000000000 ) ) ;
#5111=CARTESIAN_POINT ( 'NONE',  ( 25.00000000000000000, 0.000000000000000000, 0.000000000000000000 ) ) ;
#5113=CARTESIAN_POINT ( 'NONE',  ( 23.86937280323380506, -10.00000000000000178, -12.00000000000000000 ) ) ;
#5114=ORIENTED_EDGE ( 'NONE', *, *, #6371, .F. ) ;
#5125=AXIS2_PLACEMENT_3D ( 'NONE', #6203, #8811, #5621 ) ;
#5128=ADVANCED_FACE ( 'NONE', ( #5507 ), #1381, .F. ) ;
#5132=ORIENTED_EDGE ( 'NONE', *, *, #457, .T. ) ;
#5134=DIRECTION ( 'NONE',  ( 0.3420201433256627732, -0.9396926207859105373, 0.000000000000000000 ) ) ;
#5143=EDGE_CURVE ( 'NONE', #4307, #1402, #2922, .T. ) ;
#5145=DIRECTION ( 'NONE',  ( 0.3420201433256627732, 0.9396926207859105373, 0.000000000000000000 ) ) ;
#5147=DIRECTION ( 'NONE',  ( 0.000000000000000000, 0.000000000000000000, 1.000000000000000000 ) ) ;
#5152=VECTOR ( 'NONE', #2445, 1000.000000000000000 ) ;
#5155=ORIENTED_EDGE ( 'NONE', *, *, #468, .T. ) ;
#5156=LINE ( 'NONE', #2726, #777 ) ;
#5165=ORIENTED_EDGE ( 'NONE', *, *, #6723, .F. ) ;
#5168=LINE ( 'NONE', #1144, #2126 ) ;
#5169=VECTOR ( 'NONE', #2247, 1000.000000000000000 ) ;
#5171=ORIENTED_EDGE ( 'NONE', *, *, #8874, .F. ) ;
#5175=EDGE_LOOP ( 'NONE', ( #4058, #3790, #8150, #7322 ) ) ;
#5178=VECTOR ( 'NONE', #7370, 1000.000000000000000 ) ;
#5189=ORIENTED_EDGE ( 'NONE', *, *, #1022, .F. ) ;
#5191=EDGE_CURVE ( 'NONE', #7286, #6012, #10206, .T. ) ;
#5192=EDGE_CURVE ( 'NONE', #3788, #3797, #4563, .T. ) ;
#5201=EDGE_CURVE ( 'NONE', #3542, #1643, #7757, .T. ) ;
#5204=ORIENTED_EDGE ( 'NONE', *, *, #4410, .F. ) ;
#5207=DIRECTION ( 'NONE',  ( 0.000000000000000000, 0.000000000000000000, -1.000000000000000000 ) ) ;
#5210=CARTESIAN_POINT ( 'NONE',  ( 7.206705994753384914, 8.623026469197982991, 0.000000000000000000 ) ) ;
#5216=ORIENTED_EDGE ( 'NONE', *, *, #3704, .F. ) ;
#5220=ORIENTED_EDGE ( 'NONE', *, *, #1982, .T. ) ;
#5227=DIRECTION ( 'NONE',  ( 0.000000000000000000, -0.000000000000000000, 1.000000000000000000 ) ) ;
#5228=PRODUCT_DEFINITION_CONTEXT ( 'detailed design', #8714, 'design' ) ;
#5229=EDGE_CURVE ( 'NONE', #2398, #1402, #5264, .T. ) ;
#5233=LINE ( 'NONE', #9379, #265 ) ;
#5238=EDGE_CURVE ( 'NONE', #10028, #2670, #7814, .T. ) ;
#5239=LINE ( 'NONE', #7787, #9907 ) ;
#5242=ORIENTED_EDGE ( 'NONE', *, *, #3400, .F. ) ;
#5250=CARTESIAN_POINT ( 'NONE',  ( 9.869213319667256457, 3.750000000000000000, -12.00000000000000000 ) ) ;
#5251=EDGE_CURVE ( 'NONE', #8930, #10490, #3721, .T. ) ;
#5253=FACE_OUTER_BOUND ( 'NONE', #1967, .T. ) ;
#5254=EDGE_CURVE ( 'NONE', #244, #6381, #2141, .T. ) ;
#5258=VECTOR ( 'NONE', #5637, 1000.000000000000000 ) ;
#5259=VECTOR ( 'NONE', #1884, 1000.000000000000000 ) ;
#5264=LINE ( 'NONE', #8555, #7461 ) ;
#5268=DIRECTION ( 'NONE',  ( 0.000000000000000000, 0.000000000000000000, -1.000000000000000000 ) ) ;
#5285=DIRECTION ( 'NONE',  ( 0.3420201433256627732, -0.9396926207859105373, 0.000000000000000000 ) ) ;
#5286=SURFACE_SIDE_STYLE ('',( #6818 ) ) ;
#5289=PLANE ( 'NONE',  #1696 ) ;
#5295=VERTEX_POINT ( 'NONE', #5412 ) ;
#5297=VECTOR ( 'NONE', #895, 1000.000000000000000 ) ;
#5298=DIRECTION ( 'NONE',  ( -1.000000000000000000, -0.000000000000000000, -0.000000000000000000 ) ) ;
#5299=CARTESIAN_POINT ( 'NONE',  ( 15.26352788033274699, -7.750000000000000000, -12.00000000000000000 ) ) ;
#5301=CARTESIAN_POINT ( 'NONE',  ( 16.15239861966725599, 3.750000000000000000, -12.00000000000000000 ) ) ;
#5304=DIRECTION ( 'NONE',  ( 0.000000000000000000, -1.000000000000000000, 0.000000000000000000 ) ) ;
#5315=LINE ( 'NONE', #4356, #9593 ) ;
#5316=CARTESIAN_POINT ( 'NONE',  ( 0.000000000000000000, 6.000000000000000000, -12.00000000000000000 ) ) ;
#5318=CARTESIAN_POINT ( 'NONE',  ( 16.97133164676619899, 6.000000000000000888, 0.000000000000000000 ) ) ;
#5320=EDGE_CURVE ( 'NONE', #1744, #5526, #594, .T. ) ;
#5322=EDGE_CURVE ( 'NONE', #10163, #8333, #9294, .T. ) ;
#5324=ORIENTED_EDGE ( 'NONE', *, *, #8576, .F. ) ;
#5325=ORIENTED_EDGE ( 'NONE', *, *, #4277, .F. ) ;
#5327=VECTOR ( 'NONE', #7914, 1000.000000000000000 ) ;
#5329=ORIENTED_EDGE ( 'NONE', *, *, #10232, .F. ) ;
#5331=DIRECTION ( 'NONE',  ( 0.000000000000000000, 1.000000000000000000, 0.000000000000000000 ) ) ;
#5332=VERTEX_POINT ( 'NONE', #4460 ) ;
#5333=PLANE ( 'NONE',  #9169 ) ;
#5336=ORIENTED_EDGE ( 'NONE', *, *, #9217, .T. ) ;
#5337=EDGE_LOOP ( 'NONE', ( #9317, #9793, #44, #3686 ) ) ;
#5343=DIRECTION ( 'NONE',  ( 0.000000000000000000, 0.000000000000000000, 1.000000000000000000 ) ) ;
#5345=ORIENTED_EDGE ( 'NONE', *, *, #83, .F. ) ;
#5346=CARTESIAN_POINT ( 'NONE',  ( 11.30300220323380600, 6.000000000000000000, 0.000000000000000000 ) ) ;
#5347=CARTESIAN_POINT ( 'NONE',  ( 6.727620669667255804, -7.750000000000000000, -12.00000000000000000 ) ) ;
#5351=DIRECTION ( 'NONE',  ( -0.000000000000000000, -0.000000000000000000, 1.000000000000000000 ) ) ;
#5352=DIRECTION ( 'NONE',  ( 0.000000000000000000, -0.000000000000000000, 1.000000000000000000 ) ) ;
#5364=DIRECTION ( 'NONE',  ( 0.9396926207859105373, -0.3420201433256627732, 0.000000000000000000 ) ) ;
#5365=ORIENTED_EDGE ( 'NONE', *, *, #4095, .T. ) ;
#5368=LINE ( 'NONE', #7117, #4744 ) ;
#5378=EDGE_CURVE ( 'NONE', #6291, #307, #8130, .T. ) ;
#5380=ORIENTED_EDGE ( 'NONE', *, *, #3838, .T. ) ;
#5381=CARTESIAN_POINT ( 'NONE',  ( 23.25451694676619496, 6.000000000000000000, -12.00000000000000000 ) ) ;
#5384=ORIENTED_EDGE ( 'NONE', *, *, #6615, .T. ) ;
#5385=CARTESIAN_POINT ( 'NONE',  ( 7.546553696766196140, 6.000000000000000000, -12.00000000000000000 ) ) ;
#5386=VECTOR ( 'NONE', #4555, 1000.000000000000000 ) ;
#5390=CARTESIAN_POINT ( 'NONE',  ( 0.000000000000000000, -7.750000000000000000, -12.00000000000000000 ) ) ;
#5391=PLANE ( 'NONE',  #9884 ) ;
#5393=ORIENTED_EDGE ( 'NONE', *, *, #5886, .T. ) ;
#5394=LINE ( 'NONE', #578, #6942 ) ;
#5404=DIRECTION ( 'NONE',  ( 0.000000000000000000, -0.000000000000000000, 1.000000000000000000 ) ) ;
#5412=CARTESIAN_POINT ( 'NONE',  ( 20.72778015323380885, 6.000000000000000000, 0.000000000000000000 ) ) ;
#5414=CARTESIAN_POINT ( 'NONE',  ( 23.86937280323380506, 6.000000000000000000, -12.00000000000000000 ) ) ;
#5415=CARTESIAN_POINT ( 'NONE',  ( 16.15239861966725599, 3.750000000000000000, -12.00000000000000000 ) ) ;
#5416=CARTESIAN_POINT ( 'NONE',  ( 9.980802115791359341, 9.632714884249118370, 0.000000000000000000 ) ) ;
#5418=VECTOR ( 'NONE', #1504, 1000.000000000000000 ) ;
#5420=EDGE_CURVE ( 'NONE', #7594, #7022, #3088, .T. ) ;
#5430=ORIENTED_EDGE ( 'NONE', *, *, #628, .F. ) ;
#5432=VECTOR ( 'NONE', #8727, 1000.000000000000000 ) ;
#5434=ORIENTED_EDGE ( 'NONE', *, *, #1388, .T. ) ;
#5436=ORIENTED_EDGE ( 'NONE', *, *, #7643, .T. ) ;
#5437=FACE_OUTER_BOUND ( 'NONE', #3006, .T. ) ;
#5440=ORIENTED_EDGE ( 'NONE', *, *, #2418, .F. ) ;
#5448=LINE ( 'NONE', #8488, #1878 ) ;
#5450=EDGE_CURVE ( 'NONE', #10028, #8730, #3875, .T. ) ;
#5452=ADVANCED_FACE ( 'NONE', ( #8080 ), #9622, .F. ) ;
#5453=PRODUCT ( 'rack_ISO - Rack-spur - rectangular 1M 20PA 12FW 5PH 25L---SAll', 'rack_ISO - Rack-spur - rectangular 1M 20PA 12FW 5PH 25L---SAll', '', ( #9726 ) ) ;
#5458=DIRECTION ( 'NONE',  ( 0.3420201433256627732, 0.9396926207859105373, 0.000000000000000000 ) ) ;
#5464=ORIENTED_EDGE ( 'NONE', *, *, #8079, .F. ) ;
#5468=PLANE ( 'NONE',  #5596 ) ;
#5469=CARTESIAN_POINT ( 'NONE',  ( 25.00000000000000000, -4.000000000000000000, -10.00000000000000000 ) ) ;
#5484=CARTESIAN_POINT ( 'NONE',  ( 4.432609873715410487, 7.613338054146847611, 0.000000000000000000 ) ) ;
#5486=ORIENTED_EDGE ( 'NONE', *, *, #10406, .F. ) ;
#5487=LINE ( 'NONE', #7934, #878 ) ;
#5494=LINE ( 'NONE', #6342, #6592 ) ;
#5497=DIRECTION ( 'NONE',  ( 0.3420201433256627732, 0.9396926207859105373, -0.000000000000000000 ) ) ;
#5500=VECTOR ( 'NONE', #6447, 1000.000000000000000 ) ;
#5502=EDGE_CURVE ( 'NONE', #6626, #4690, #3247, .T. ) ;
#5503=CARTESIAN_POINT ( 'NONE',  ( 4.404961046766194599, -10.00000000000000000, -12.00000000000000000 ) ) ;
#5507=FACE_OUTER_BOUND ( 'NONE', #10115, .T. ) ;
#5517=PLANE ( 'NONE',  #4116 ) ;
#5521=DIRECTION ( 'NONE',  ( -1.000000000000000000, 0.000000000000000000, -0.000000000000000000 ) ) ;
#5522=DIRECTION ( 'NONE',  ( 0.000000000000000000, -0.000000000000000000, -1.000000000000000000 ) ) ;
#5524=CARTESIAN_POINT ( 'NONE',  ( 25.00000000000000000, -4.000000000000000000, -12.00000000000000000 ) ) ;
#5525=PLANE ( 'NONE',  #6612 ) ;
#5526=VERTEX_POINT ( 'NONE', #5301 ) ;
#5538=LINE ( 'NONE', #9428, #9131 ) ;
#5542=ORIENTED_EDGE ( 'NONE', *, *, #705, .T. ) ;
#5545=DIRECTION ( 'NONE',  ( 0.000000000000000000, 0.000000000000000000, 1.000000000000000000 ) ) ;
#5551=EDGE_LOOP ( 'NONE', ( #10074, #842, #95, #4383 ) ) ;
#5555=VERTEX_POINT ( 'NONE', #7697 ) ;
#5559=LINE ( 'NONE', #8803, #8131 ) ;
#5564=CARTESIAN_POINT ( 'NONE',  ( 1.878224253233806040, 6.000000000000000000, -12.00000000000000000 ) ) ;
#5566=PLANE ( 'NONE',  #5125 ) ;
#5570=FACE_OUTER_BOUND ( 'NONE', #8478, .T. ) ;
#5572=VECTOR ( 'NONE', #473, 1000.000000000000000 ) ;
#5577=CARTESIAN_POINT ( 'NONE',  ( 1.868979409283444415, 6.025400000000000311, -12.00000000000000000 ) ) ;
#5581=ORIENTED_EDGE ( 'NONE', *, *, #10232, .T. ) ;
#5582=EDGE_CURVE ( 'NONE', #7195, #6101, #1277, .T. ) ;
#5588=EDGE_LOOP ( 'NONE', ( #5608, #4334, #4846, #5365 ) ) ;
#5592=DIRECTION ( 'NONE',  ( -0.000000000000000000, -0.000000000000000000, 1.000000000000000000 ) ) ;
#5593=ORIENTED_EDGE ( 'NONE', *, *, #6848, .T. ) ;
#5596=AXIS2_PLACEMENT_3D ( 'NONE', #6955, #493, #10207 ) ;
#5597=ORIENTED_EDGE ( 'NONE', *, *, #4802, .F. ) ;
#5602=CARTESIAN_POINT ( 'NONE',  ( 20.11292429676619520, -10.00000000000000000, -12.00000000000000000 ) ) ;
#5608=ORIENTED_EDGE ( 'NONE', *, *, #4911, .T. ) ;
#5610=DIRECTION ( 'NONE',  ( 0.000000000000000000, 0.000000000000000000, 1.000000000000000000 ) ) ;
#5612=CARTESIAN_POINT ( 'NONE',  ( 0.000000000000000000, -10.00000000000000000, -12.00000000000000000 ) ) ;
#5613=CARTESIAN_POINT ( 'NONE',  ( 12.12193523033274545, -7.750000000000000000, 0.000000000000000000 ) ) ;
#5615=DIRECTION ( 'NONE',  ( 0.9396926207859105373, 0.3420201433256627732, 0.000000000000000000 ) ) ;
#5621=DIRECTION ( 'NONE',  ( 0.3420201433256627732, -0.9396926207859105373, 0.000000000000000000 ) ) ;
#5624=LINE ( 'NONE', #2460, #9767 ) ;
#5627=CARTESIAN_POINT ( 'NONE',  ( 3.586028019667255595, -7.750000000000000000, 0.000000000000000000 ) ) ;
#5631=EDGE_CURVE ( 'NONE', #5003, #2005, #433, .T. ) ;
#5635=ORIENTED_EDGE ( 'NONE', *, *, #9432, .T. ) ;
#5637=DIRECTION ( 'NONE',  ( -1.000000000000000000, 0.000000000000000000, -0.000000000000000000 ) ) ;
#5642=EDGE_CURVE ( 'NONE', #4597, #789, #7747, .T. ) ;
#5647=ORIENTED_EDGE ( 'NONE', *, *, #796, .F. ) ;
#5650=ORIENTED_EDGE ( 'NONE', *, *, #6334, .F. ) ;
#5652=LINE ( 'NONE', #2323, #173 ) ;
#5655=DIRECTION ( 'NONE',  ( -0.3420201433256627732, -0.9396926207859105373, 0.000000000000000000 ) ) ;
#5657=EDGE_LOOP ( 'NONE', ( #3719, #3668, #3524, #1416 ) ) ;
#5667=LINE ( 'NONE', #1707, #4755 ) ;
#5670=CARTESIAN_POINT ( 'NONE',  ( 1.878224253233805818, -10.00000000000000000, -12.00000000000000000 ) ) ;
#5676=FACE_OUTER_BOUND ( 'NONE', #6494, .T. ) ;
#5678=CARTESIAN_POINT ( 'NONE',  ( 24.68830583033274806, 3.750000000000000000, -12.00000000000000000 ) ) ;
#5680=DIRECTION ( 'NONE',  ( -0.3420201433256627732, 0.9396926207859105373, 0.000000000000000000 ) ) ;
#5684=ORIENTED_EDGE ( 'NONE', *, *, #7077, .F. ) ;
#5685=ORIENTED_EDGE ( 'NONE', *, *, #8455, .F. ) ;
#5686=DIRECTION ( 'NONE',  ( -0.000000000000000000, -0.000000000000000000, 1.000000000000000000 ) ) ;
#5691=DIRECTION ( 'NONE',  ( -0.000000000000000000, 0.000000000000000000, -1.000000000000000000 ) ) ;
#5694=VERTEX_POINT ( 'NONE', #3180 ) ;
#5697=EDGE_CURVE ( 'NONE', #8159, #6209, #4820, .T. ) ;
#5698=( LENGTH_UNIT ( ) NAMED_UNIT ( * ) SI_UNIT ( .MILLI., .METRE. ) );
#5701=PLANE ( 'NONE',  #4980 ) ;
#5709=CARTESIAN_POINT ( 'NONE',  ( 20.12216914071655793, -10.02539999999999942, -12.00000000000000000 ) ) ;
#5719=ADVANCED_FACE ( 'NONE', ( #57 ), #3232, .F. ) ;
#5727=LINE ( 'NONE', #7279, #3036 ) ;
#5735=LINE ( 'NONE', #87, #2736 ) ;
#5736=VECTOR ( 'NONE', #1664, 1000.000000000000000 ) ;
#5738=EDGE_CURVE ( 'NONE', #1584, #10233, #799, .T. ) ;
#5749=VERTEX_POINT ( 'NONE', #7093 ) ;
#5750=CARTESIAN_POINT ( 'NONE',  ( 0.000000000000000000, -4.000000000000000000, 0.000000000000000000 ) ) ;
#5753=ORIENTED_EDGE ( 'NONE', *, *, #7107, .F. ) ;
#5761=VECTOR ( 'NONE', #9180, 1000.000000000000000 ) ;
#5767=DIRECTION ( 'NONE',  ( 0.3420201433256627732, -0.9396926207859105373, 0.000000000000000000 ) ) ;
#5770=ORIENTED_EDGE ( 'NONE', *, *, #9849, .T. ) ;
#5775=DIRECTION ( 'NONE',  ( -1.000000000000000000, 0.000000000000000000, -0.000000000000000000 ) ) ;
#5777=DIRECTION ( 'NONE',  ( 0.000000000000000000, -1.000000000000000000, 0.000000000000000000 ) ) ;
#5779=DIRECTION ( 'NONE',  ( 0.3420201433256627732, -0.9396926207859105373, 0.000000000000000000 ) ) ;
#5782=LINE ( 'NONE', #6581, #1686 ) ;
#5783=EDGE_CURVE ( 'NONE', #4315, #1597, #1598, .T. ) ;
#5789=FACE_OUTER_BOUND ( 'NONE', #785, .T. ) ;
#5790=CARTESIAN_POINT ( 'NONE',  ( 1.658513752677435171, -10.60364963909571401, 0.000000000000000000 ) ) ;
#5795=ORIENTED_EDGE ( 'NONE', *, *, #3227, .T. ) ;
#5800=ORIENTED_EDGE ( 'NONE', *, *, #2088, .F. ) ;
#5811=( LENGTH_UNIT ( ) NAMED_UNIT ( * ) SI_UNIT ( .MILLI., .METRE. ) );
#5814=FACE_OUTER_BOUND ( 'NONE', #10062, .T. ) ;
#5818=VECTOR ( 'NONE', #5343, 1000.000000000000000 ) ;
#5820=EDGE_CURVE ( 'NONE', #2302, #3003, #4872, .T. ) ;
#5823=ORIENTED_EDGE ( 'NONE', *, *, #10433, .F. ) ;
#5831=PLANE ( 'NONE',  #108 ) ;
#5832=ADVANCED_FACE ( 'NONE', ( #7476 ), #901, .F. ) ;
#5836=AXIS2_PLACEMENT_3D ( 'NONE', #6391, #9541, #3167 ) ;
#5844=VERTEX_POINT ( 'NONE', #267 ) ;
#5846=CARTESIAN_POINT ( 'NONE',  ( 1.878224253233806040, -10.00000000000000000, -12.00000000000000000 ) ) ;
#5848=VERTEX_POINT ( 'NONE', #2695 ) ;
#5851=ORIENTED_EDGE ( 'NONE', *, *, #2618, .F. ) ;
#5854=DIRECTION ( 'NONE',  ( 1.000000000000000000, 0.000000000000000000, 0.000000000000000000 ) ) ;
#5855=PRESENTATION_STYLE_ASSIGNMENT (( #4118 ) ) ;
#5864=DIRECTION ( 'NONE',  ( -1.000000000000000000, -0.000000000000000000, -0.000000000000000000 ) ) ;
#5872=EDGE_LOOP ( 'NONE', ( #4561, #1825, #5436, #6450 ) ) ;
#5874=DIRECTION ( 'NONE',  ( -0.9396926207859105373, 0.3420201433256627732, 0.000000000000000000 ) ) ;
#5879=DIRECTION ( 'NONE',  ( 0.000000000000000000, -1.000000000000000000, 0.000000000000000000 ) ) ;
#5885=ORIENTED_EDGE ( 'NONE', *, *, #7389, .F. ) ;
#5886=EDGE_CURVE ( 'NONE', #8274, #10315, #1748, .T. ) ;
#5890=VERTEX_POINT ( 'NONE', #8956 ) ;
#5895=EDGE_CURVE ( 'NONE', #4888, #1146, #7523, .T. ) ;
#5899=ORIENTED_EDGE ( 'NONE', *, *, #2416, .T. ) ;
#5905=EDGE_LOOP ( 'NONE', ( #5329, #5132, #4586, #86 ) ) ;
#5912=ADVANCED_FACE ( 'NONE', ( #5814 ), #8170, .T. ) ;
#5918=ORIENTED_EDGE ( 'NONE', *, *, #5378, .T. ) ;
#5922=EDGE_LOOP ( 'NONE', ( #2253, #6221, #5380, #8110 ) ) ;
#5928=CARTESIAN_POINT ( 'NONE',  ( 0.000000000000000000, -7.750000000000000000, -12.00000000000000000 ) ) ;
#5933=AXIS2_PLACEMENT_3D ( 'NONE', #9949, #9041, #9742 ) ;
#5939=ORIENTED_EDGE ( 'NONE', *, *, #6284, .T. ) ;
#5956=EDGE_CURVE ( 'NONE', #3378, #4582, #1908, .T. ) ;
#5959=ORIENTED_EDGE ( 'NONE', *, *, #7937, .T. ) ;
#5962=( NAMED_UNIT ( * ) PLANE_ANGLE_UNIT ( ) SI_UNIT ( $, .RADIAN. ) );
#5964=CARTESIAN_POINT ( 'NONE',  ( 9.869213319667256457, 3.750000000000000000, 0.000000000000000000 ) ) ;
#5968=LINE ( 'NONE', #1962, #10160 ) ;
#5973=EDGE_LOOP ( 'NONE', ( #5440, #4967, #515, #4437 ) ) ;
#6002=VECTOR ( 'NONE', #8819, 1000.000000000000000 ) ;
#6003=EDGE_CURVE ( 'NONE', #3335, #4690, #5233, .T. ) ;
#6008=ORIENTED_EDGE ( 'NONE', *, *, #5254, .T. ) ;
#6012=VERTEX_POINT ( 'NONE', #6820 ) ;
#6016=EDGE_CURVE ( 'NONE', #3392, #2266, #3646, .T. ) ;
#6017=EDGE_CURVE ( 'NONE', #9702, #10315, #3694, .T. ) ;
#6018=EDGE_LOOP ( 'NONE', ( #3990, #6126, #7484, #8436 ) ) ;
#6019=PLANE ( 'NONE',  #9411 ) ;
#6020=DIRECTION ( 'NONE',  ( 0.000000000000000000, -1.000000000000000000, -0.000000000000000000 ) ) ;
#6024=DIRECTION ( 'NONE',  ( 1.000000000000000000, 0.000000000000000000, -0.000000000000000000 ) ) ;
#6026=VERTEX_POINT ( 'NONE', #315 ) ;
#6028=DIRECTION ( 'NONE',  ( -1.000000000000000000, 0.000000000000000000, 0.000000000000000000 ) ) ;
#6038=EDGE_CURVE ( 'NONE', #4888, #1744, #1364, .T. ) ;
#6056=LINE ( 'NONE', #8468, #10003 ) ;
#6057=ORIENTED_EDGE ( 'NONE', *, *, #4526, .F. ) ;
#6064=ADVANCED_FACE ( 'NONE', ( #6181 ), #6019, .T. ) ;
#6068=VECTOR ( 'NONE', #1887, 1000.000000000000000 ) ;
#6069=ORIENTED_EDGE ( 'NONE', *, *, #457, .F. ) ;
#6076=DIRECTION ( 'NONE',  ( 0.3420201433256627732, -0.9396926207859105373, 0.000000000000000000 ) ) ;
#6081=DIRECTION ( 'NONE',  ( -0.000000000000000000, -0.000000000000000000, 1.000000000000000000 ) ) ;
#6083=VECTOR ( 'NONE', #551, 1000.000000000000000 ) ;
#6085=DIRECTION ( 'NONE',  ( 0.000000000000000000, 0.000000000000000000, 1.000000000000000000 ) ) ;
#6089=VECTOR ( 'NONE', #7043, 1000.000000000000000 ) ;
#6101=VERTEX_POINT ( 'NONE', #5964 ) ;
#6107=ORIENTED_EDGE ( 'NONE', *, *, #5143, .F. ) ;
#6112=ORIENTED_EDGE ( 'NONE', *, *, #7138, .F. ) ;
#6120=CARTESIAN_POINT ( 'NONE',  ( 5.019816903233806471, -10.00000000000000000, 0.000000000000000000 ) ) ;
#6121=ORIENTED_EDGE ( 'NONE', *, *, #5820, .F. ) ;
#6126=ORIENTED_EDGE ( 'NONE', *, *, #5895, .T. ) ;
#6128=LINE ( 'NONE', #3798, #9143 ) ;
#6131=DIRECTION ( 'NONE',  ( 0.3420201433256627732, 0.9396926207859105373, 0.000000000000000000 ) ) ;
#6134=DIRECTION ( 'NONE',  ( 1.000000000000000000, 0.000000000000000000, 0.000000000000000000 ) ) ;
#6143=LINE ( 'NONE', #2128, #7209 ) ;
#6144=DIRECTION ( 'NONE',  ( 0.000000000000000000, 0.000000000000000000, 1.000000000000000000 ) ) ;
#6145=LINE ( 'NONE', #8546, #5386 ) ;
#6150=ORIENTED_EDGE ( 'NONE', *, *, #8229, .F. ) ;
#6152=CARTESIAN_POINT ( 'NONE',  ( 2.697157280332745266, 3.750000000000000000, -12.00000000000000000 ) ) ;
#6155=LINE ( 'NONE', #1446, #7976 ) ;
#6156=LINE ( 'NONE', #3723, #10192 ) ;
#6157=CARTESIAN_POINT ( 'NONE',  ( 1.868979409283444415, -10.02539999999999942, -12.00000000000000000 ) ) ;
#6158=ORIENTED_EDGE ( 'NONE', *, *, #5420, .F. ) ;
#6164=VERTEX_POINT ( 'NONE', #7734 ) ;
#6168=VECTOR ( 'NONE', #7627, 1000.000000000000000 ) ;
#6169=CARTESIAN_POINT ( 'NONE',  ( 25.00000000000000000, -4.000000000000000000, 0.000000000000000000 ) ) ;
#6175=PLANE ( 'NONE',  #1888 ) ;
#6181=FACE_OUTER_BOUND ( 'NONE', #8853, .T. ) ;
#6182=CARTESIAN_POINT ( 'NONE',  ( 22.43558391966725907, 3.750000000000000000, -12.00000000000000000 ) ) ;
#6184=CARTESIAN_POINT ( 'NONE',  ( 19.29399126966725575, 3.750000000000000000, 0.000000000000000000 ) ) ;
#6188=ORIENTED_EDGE ( 'NONE', *, *, #4277, .T. ) ;
#6189=AXIS2_PLACEMENT_3D ( 'NONE', #4400, #7586, #3609 ) ;
#6195=DIRECTION ( 'NONE',  ( -0.9396926207859105373, 0.3420201433256627732, 0.000000000000000000 ) ) ;
#6201=ADVANCED_FACE ( 'NONE', ( #10282 ), #10394, .F. ) ;
#6203=CARTESIAN_POINT ( 'NONE',  ( 11.29375735928344504, 6.025400000000000311, -12.00000000000000000 ) ) ;
#6207=DIRECTION ( 'NONE',  ( 1.000000000000000000, 0.000000000000000000, -0.000000000000000000 ) ) ;
#6209=VERTEX_POINT ( 'NONE', #5602 ) ;
#6214=VERTEX_POINT ( 'NONE', #7939 ) ;
#6216=CARTESIAN_POINT ( 'NONE',  ( 4.404961046766194599, 6.000000000000000000, -12.00000000000000000 ) ) ;
#6221=ORIENTED_EDGE ( 'NONE', *, *, #5886, .F. ) ;
#6222=EDGE_CURVE ( 'NONE', #1785, #6919, #1586, .T. ) ;
#6228=ADVANCED_FACE ( 'NONE', ( #6340 ), #8681, .F. ) ;
#6232=LINE ( 'NONE', #8684, #8799 ) ;
#6237=LINE ( 'NONE', #3657, #9852 ) ;
#6240=DIRECTION ( 'NONE',  ( 1.000000000000000000, 0.000000000000000000, 0.000000000000000000 ) ) ;
#6242=DIRECTION ( 'NONE',  ( 0.3420201433256627732, 0.9396926207859105373, 0.000000000000000000 ) ) ;
#6244=PLANE ( 'NONE',  #9080 ) ;
#6246=VECTOR ( 'NONE', #4978, 1000.000000000000000 ) ;
#6247=CARTESIAN_POINT ( 'NONE',  ( 0.000000000000000000, 6.000000000000000000, -12.00000000000000000 ) ) ;
#6253=DIRECTION ( 'NONE',  ( -1.000000000000000000, -0.000000000000000000, -0.000000000000000000 ) ) ;
#6256=VECTOR ( 'NONE', #8768, 1000.000000000000000 ) ;
#6257=CARTESIAN_POINT ( 'NONE',  ( 0.000000000000000000, -10.00000000000000000, -12.00000000000000000 ) ) ;
#6259=FACE_OUTER_BOUND ( 'NONE', #5337, .T. ) ;
#6263=CARTESIAN_POINT ( 'NONE',  ( 25.00000000000000000, 0.000000000000000000, -12.00000000000000000 ) ) ;
#6266=AXIS2_PLACEMENT_3D ( 'NONE', #4289, #3399, #2658 ) ;
#6270=VECTOR ( 'NONE', #2878, 1000.000000000000000 ) ;
#6271=AXIS2_PLACEMENT_3D ( 'NONE', #2509, #4336, #6473 ) ;
#6272=ORIENTED_EDGE ( 'NONE', *, *, #1753, .T. ) ;
#6276=ORIENTED_EDGE ( 'NONE', *, *, #3517, .F. ) ;
#6284=EDGE_CURVE ( 'NONE', #5844, #2608, #7080, .T. ) ;
#6286=EDGE_CURVE ( 'NONE', #4950, #5295, #7135, .T. ) ;
#6291=VERTEX_POINT ( 'NONE', #4694 ) ;
#6293=DIRECTION ( 'NONE',  ( 0.000000000000000000, 0.000000000000000000, -1.000000000000000000 ) ) ;
#6294=ORIENTED_EDGE ( 'NONE', *, *, #5191, .T. ) ;
#6297=DIRECTION ( 'NONE',  ( 0.3420201433256627732, -0.9396926207859105373, 0.000000000000000000 ) ) ;
#6300=VECTOR ( 'NONE', #5298, 1000.000000000000000 ) ;
#6306=VERTEX_POINT ( 'NONE', #10335 ) ;
#6310=ORIENTED_EDGE ( 'NONE', *, *, #10446, .T. ) ;
#6311=DIRECTION ( 'NONE',  ( -0.000000000000000000, 1.000000000000000000, 0.000000000000000000 ) ) ;
#6325=CARTESIAN_POINT ( 'NONE',  ( 6.727620669667255804, 3.750000000000000000, -12.00000000000000000 ) ) ;
#6329=CARTESIAN_POINT ( 'NONE',  ( 8.980342580332745683, -7.750000000000000000, 0.000000000000000000 ) ) ;
#6330=FACE_OUTER_BOUND ( 'NONE', #4054, .T. ) ;
#6334=EDGE_CURVE ( 'NONE', #4307, #9203, #8786, .T. ) ;
#6338=APPLICATION_CONTEXT ( 'automotive_design' ) ;
#6340=FACE_OUTER_BOUND ( 'NONE', #833, .T. ) ;
#6341=PRODUCT_DEFINITION_FORMATION_WITH_SPECIFIED_SOURCE ( 'ANY', '', #5453, .NOT_KNOWN. ) ;
#6342=CARTESIAN_POINT ( 'NONE',  ( 22.43558391966725907, -7.750000000000000000, -12.00000000000000000 ) ) ;
#6345=CARTESIAN_POINT ( 'NONE',  ( 10.69739119071655686, -10.02539999999999942, 0.000000000000000000 ) ) ;
#6352=DIRECTION ( 'NONE',  ( 0.000000000000000000, 0.000000000000000000, 1.000000000000000000 ) ) ;
#6358=DIRECTION ( 'NONE',  ( -1.000000000000000000, 0.000000000000000000, 0.000000000000000000 ) ) ;
#6370=ORIENTED_EDGE ( 'NONE', *, *, #9355, .T. ) ;
#6371=EDGE_CURVE ( 'NONE', #4487, #5555, #8161, .T. ) ;
#6372=FACE_OUTER_BOUND ( 'NONE', #9438, .T. ) ;
#6374=CARTESIAN_POINT ( 'NONE',  ( 9.980802115791359341, -13.63271488424911837, 0.000000000000000000 ) ) ;
#6381=VERTEX_POINT ( 'NONE', #1842 ) ;
#6383=ORIENTED_EDGE ( 'NONE', *, *, #1658, .F. ) ;
#6384=LINE ( 'NONE', #8046, #2018 ) ;
#6387=CARTESIAN_POINT ( 'NONE',  ( 20.11292429676619520, 6.000000000000000000, -12.00000000000000000 ) ) ;
#6391=CARTESIAN_POINT ( 'NONE',  ( 5.010572059283444624, -10.02539999999999942, -12.00000000000000000 ) ) ;
#6392=DIRECTION ( 'NONE',  ( 0.3420201433256627732, -0.9396926207859105373, 0.000000000000000000 ) ) ;
#6395=EDGE_CURVE ( 'NONE', #4407, #138, #4267, .T. ) ;
#6401=CARTESIAN_POINT ( 'NONE',  ( 0.000000000000000000, -10.00000000000000000, -12.00000000000000000 ) ) ;
#6405=ADVANCED_FACE ( 'NONE', ( #1792 ), #3275, .T. ) ;
#6409=VECTOR ( 'NONE', #10384, 1000.000000000000000 ) ;
#6411=AXIS2_PLACEMENT_3D ( 'NONE', #2549, #2394, #5767 ) ;
#6413=LINE ( 'NONE', #9671, #7680 ) ;
#6419=CARTESIAN_POINT ( 'NONE',  ( 8.161409553233806236, 6.000000000000000000, -12.00000000000000000 ) ) ;
#6428=AXIS2_PLACEMENT_3D ( 'NONE', #934, #5691, #9747 ) ;
#6430=ORIENTED_EDGE ( 'NONE', *, *, #2220, .F. ) ;
#6436=ORIENTED_EDGE ( 'NONE', *, *, #2136, .T. ) ;
#6437=VECTOR ( 'NONE', #3772, 1000.000000000000000 ) ;
#6439=VECTOR ( 'NONE', #6134, 1000.000000000000000 ) ;
#6440=VERTEX_POINT ( 'NONE', #146 ) ;
#6447=DIRECTION ( 'NONE',  ( 0.3420201433256627732, -0.9396926207859105373, 0.000000000000000000 ) ) ;
#6448=CARTESIAN_POINT ( 'NONE',  ( 4.414205890716556446, -10.02539999999999942, -12.00000000000000000 ) ) ;
#6450=ORIENTED_EDGE ( 'NONE', *, *, #5143, .T. ) ;
#6454=ORIENTED_EDGE ( 'NONE', *, *, #2609, .F. ) ;
#6457=VERTEX_POINT ( 'NONE', #9106 ) ;
#6460=CARTESIAN_POINT ( 'NONE',  ( 25.00000000000000000, -4.000000000000000000, -2.000000000000000000 ) ) ;
#6472=CARTESIAN_POINT ( 'NONE',  ( 18.30309047890528618, -16.66178012940252273, 0.000000000000000000 ) ) ;
#6473=DIRECTION ( 'NONE',  ( 0.000000000000000000, 0.000000000000000000, -1.000000000000000000 ) ) ;
#6483=ORIENTED_EDGE ( 'NONE', *, *, #5229, .T. ) ;
#6491=ORIENTED_EDGE ( 'NONE', *, *, #6038, .F. ) ;
#6494=EDGE_LOOP ( 'NONE', ( #3435, #5013, #9624, #3158 ) ) ;
#6495=VECTOR ( 'NONE', #3604, 1000.000000000000000 ) ;
#6520=PLANE ( 'NONE',  #7344 ) ;
#6523=EDGE_CURVE ( 'NONE', #9213, #8065, #2637, .T. ) ;
#6526=FACE_OUTER_BOUND ( 'NONE', #10065, .T. ) ;
#6527=DIRECTION ( 'NONE',  ( -0.3420201433256627732, -0.9396926207859105373, 0.000000000000000000 ) ) ;
#6528=DIRECTION ( 'NONE',  ( 0.3420201433256627732, 0.9396926207859105373, -0.000000000000000000 ) ) ;
#6534=DIRECTION ( 'NONE',  ( 1.000000000000000000, -0.000000000000000000, -0.000000000000000000 ) ) ;
#6539=ORIENTED_EDGE ( 'NONE', *, *, #8887, .T. ) ;
#6540=PLANE ( 'NONE',  #5933 ) ;
#6544=CARTESIAN_POINT ( 'NONE',  ( 3.586028019667255595, -7.750000000000000000, -12.00000000000000000 ) ) ;
#6545=ORIENTED_EDGE ( 'NONE', *, *, #1171, .F. ) ;
#6550=ORIENTED_EDGE ( 'NONE', *, *, #1498, .F. ) ;
#6552=VERTEX_POINT ( 'NONE', #4964 ) ;
#6553=ADVANCED_FACE ( 'NONE', ( #46 ), #9755, .F. ) ;
#6561=ORIENTED_EDGE ( 'NONE', *, *, #1673, .F. ) ;
#6565=FACE_OUTER_BOUND ( 'NONE', #4155, .T. ) ;
#6573=CARTESIAN_POINT ( 'NONE',  ( 3.586028019667255595, -7.750000000000000000, -12.00000000000000000 ) ) ;
#6576=CARTESIAN_POINT ( 'NONE',  ( 1.878224253233805818, 6.000000000000000000, -12.00000000000000000 ) ) ;
#6581=CARTESIAN_POINT ( 'NONE',  ( 25.00000000000000000, -4.000000000000000000, -10.00000000000000000 ) ) ;
#6584=ORIENTED_EDGE ( 'NONE', *, *, #2859, .F. ) ;
#6588=CARTESIAN_POINT ( 'NONE',  ( 15.26352788033274699, 3.750000000000000000, -12.00000000000000000 ) ) ;
#6591=ORIENTED_EDGE ( 'NONE', *, *, #2418, .T. ) ;
#6592=VECTOR ( 'NONE', #9596, 1000.000000000000000 ) ;
#6601=AXIS2_PLACEMENT_3D ( 'NONE', #9260, #8571, #2000 ) ;
#6612=AXIS2_PLACEMENT_3D ( 'NONE', #8709, #548, #7057 ) ;
#6614=VECTOR ( 'NONE', #1163, 1000.000000000000000 ) ;
#6615=EDGE_CURVE ( 'NONE', #4686, #10490, #5168, .T. ) ;
#6616=EDGE_CURVE ( 'NONE', #4950, #2005, #8418, .T. ) ;
#6617=ORIENTED_EDGE ( 'NONE', *, *, #845, .T. ) ;
#6620=CARTESIAN_POINT ( 'NONE',  ( 4.404961046766194599, -10.00000000000000000, 0.000000000000000000 ) ) ;
#6621=DIRECTION ( 'NONE',  ( 0.000000000000000000, 0.000000000000000000, 1.000000000000000000 ) ) ;
#6626=VERTEX_POINT ( 'NONE', #2245 ) ;
#6627=LINE ( 'NONE', #10038, #5761 ) ;
#6634=DIRECTION ( 'NONE',  ( -0.3420201433256627732, -0.9396926207859105373, 0.000000000000000000 ) ) ;
#6639=ORIENTED_EDGE ( 'NONE', *, *, #8845, .F. ) ;
#6641=LINE ( 'NONE', #7444, #3243 ) ;
#6643=ORIENTED_EDGE ( 'NONE', *, *, #10008, .T. ) ;
#6645=VECTOR ( 'NONE', #7085, 1000.000000000000000 ) ;
#6650=ORIENTED_EDGE ( 'NONE', *, *, #9736, .F. ) ;
#6651=EDGE_CURVE ( 'NONE', #9748, #4597, #3089, .T. ) ;
#6654=ORIENTED_EDGE ( 'NONE', *, *, #5502, .F. ) ;
#6658=ORIENTED_EDGE ( 'NONE', *, *, #4936, .T. ) ;
#6661=VECTOR ( 'NONE', #7901, 1000.000000000000000 ) ;
#6664=DIRECTION ( 'NONE',  ( 0.000000000000000000, 1.000000000000000000, 0.000000000000000000 ) ) ;
#6665=FACE_OUTER_BOUND ( 'NONE', #472, .T. ) ;
#6669=CARTESIAN_POINT ( 'NONE',  ( 16.97133164676619899, -10.00000000000000178, 0.000000000000000000 ) ) ;
#6674=EDGE_CURVE ( 'NONE', #1096, #5848, #10013, .T. ) ;
#6678=AXIS2_PLACEMENT_3D ( 'NONE', #9778, #7971, #5521 ) ;
#6679=LINE ( 'NONE', #9937, #5008 ) ;
#6682=CARTESIAN_POINT ( 'NONE',  ( 0.000000000000000000, -10.00000000000000000, 0.000000000000000000 ) ) ;
#6697=AXIS2_PLACEMENT_3D ( 'NONE', #2924, #5304, #3559 ) ;
#6703=ORIENTED_EDGE ( 'NONE', *, *, #4812, .T. ) ;
#6706=ORIENTED_EDGE ( 'NONE', *, *, #9355, .F. ) ;
#6715=DIRECTION ( 'NONE',  ( -0.000000000000000000, -0.000000000000000000, 1.000000000000000000 ) ) ;
#6719=CARTESIAN_POINT ( 'NONE',  ( 13.83898384071655840, 6.025400000000000311, -12.00000000000000000 ) ) ;
#6723=EDGE_CURVE ( 'NONE', #8225, #5844, #1198, .T. ) ;
#6726=CARTESIAN_POINT ( 'NONE',  ( 8.980342580332745683, 3.750000000000000000, -12.00000000000000000 ) ) ;
#6740=DIRECTION ( 'NONE',  ( -0.000000000000000000, 1.000000000000000000, 0.000000000000000000 ) ) ;
#6747=CARTESIAN_POINT ( 'NONE',  ( 6.727620669667255804, -7.750000000000000000, -12.00000000000000000 ) ) ;
#6752=CARTESIAN_POINT ( 'NONE',  ( 0.000000000000000000, -4.000000000000000000, -12.00000000000000000 ) ) ;
#6764=VECTOR ( 'NONE', #6534, 1000.000000000000000 ) ;
#6767=CARTESIAN_POINT ( 'NONE',  ( 14.43535000928344481, -10.02539999999999942, -12.00000000000000000 ) ) ;
#6769=DIRECTION ( 'NONE',  ( -0.000000000000000000, -0.000000000000000000, 1.000000000000000000 ) ) ;
#6771=CARTESIAN_POINT ( 'NONE',  ( 24.68830583033274806, 3.750000000000000000, 0.000000000000000000 ) ) ;
#6774=ORIENTED_EDGE ( 'NONE', *, *, #4515, .T. ) ;
#6778=EDGE_CURVE ( 'NONE', #8930, #1347, #5624, .T. ) ;
#6786=EDGE_CURVE ( 'NONE', #8730, #2255, #8081, .T. ) ;
#6788=CARTESIAN_POINT ( 'NONE',  ( 2.697157280332745266, -7.750000000000000000, -12.00000000000000000 ) ) ;
#6791=ADVANCED_FACE ( 'NONE', ( #6526 ), #1660, .T. ) ;
#6802=EDGE_CURVE ( 'NONE', #8270, #2670, #1501, .T. ) ;
#6805=ORIENTED_EDGE ( 'NONE', *, *, #6651, .T. ) ;
#6807=ORIENTED_EDGE ( 'NONE', *, *, #6371, .T. ) ;
#6809=DIRECTION ( 'NONE',  ( 0.000000000000000000, 0.000000000000000000, -1.000000000000000000 ) ) ;
#6818=SURFACE_STYLE_FILL_AREA ( #2062 ) ;
#6820=CARTESIAN_POINT ( 'NONE',  ( 16.97133164676619899, -10.00000000000000178, -12.00000000000000000 ) ) ;
#6823=LINE ( 'NONE', #8380, #4548 ) ;
#6828=VERTEX_POINT ( 'NONE', #72 ) ;
#6830=CARTESIAN_POINT ( 'NONE',  ( 0.4444353696672553311, -7.750000000000000000, -12.00000000000000000 ) ) ;
#6832=LINE ( 'NONE', #5928, #8373 ) ;
#6835=CARTESIAN_POINT ( 'NONE',  ( 8.980342580332745683, 3.750000000000000000, -12.00000000000000000 ) ) ;
#6843=VECTOR ( 'NONE', #9172, 1000.000000000000000 ) ;
#6848=EDGE_CURVE ( 'NONE', #2931, #2005, #3935, .T. ) ;
#6849=CARTESIAN_POINT ( 'NONE',  ( 0.000000000000000000, -10.00000000000000000, -12.00000000000000000 ) ) ;
#6851=VECTOR ( 'NONE', #892, 1000.000000000000000 ) ;
#6853=CARTESIAN_POINT ( 'NONE',  ( 0.000000000000000000, 0.000000000000000000, -12.00000000000000000 ) ) ;
#6859=ORIENTED_EDGE ( 'NONE', *, *, #8247, .F. ) ;
#6861=AXIS2_PLACEMENT_3D ( 'NONE', #5095, #4451, #4295 ) ;
#6874=ADVANCED_FACE ( 'NONE', ( #5570 ), #9569, .T. ) ;
#6876=ORIENTED_EDGE ( 'NONE', *, *, #4060, .F. ) ;
#6890=LINE ( 'NONE', #10044, #4161 ) ;
#6891=LINE ( 'NONE', #4608, #2693 ) ;
#6898=LINE ( 'NONE', #596, #1037 ) ;
#6900=DIRECTION ( 'NONE',  ( 0.000000000000000000, 0.000000000000000000, 1.000000000000000000 ) ) ;
#6907=EDGE_LOOP ( 'NONE', ( #1065, #160, #3423, #1726, #3852, #4209, #6643, #1839, #364, #4023, #9154, #6550, #6383, #1961, #1552, #4753, #8783, #4639, #109, #6639, #9971, #621, #9911, #7374, #1026, #2299, #2100, #3053, #9357, #8862, #10032, #1269, #2573, #5770, #453, #5384 ) ) ;
#6909=CARTESIAN_POINT ( 'NONE',  ( 25.00000000000000000, -4.000000000000000000, -10.00000000000000000 ) ) ;
#6911=LINE ( 'NONE', #2742, #181 ) ;
#6912=ORIENTED_EDGE ( 'NONE', *, *, #4060, .T. ) ;
#6919=VERTEX_POINT ( 'NONE', #9885 ) ;
#6920=ORIENTED_EDGE ( 'NONE', *, *, #4812, .F. ) ;
#6922=VECTOR ( 'NONE', #7738, 1000.000000000000000 ) ;
#6924=VERTEX_POINT ( 'NONE', #1818 ) ;
#6925=CARTESIAN_POINT ( 'NONE',  ( 13.01080596966725622, -7.750000000000000000, -12.00000000000000000 ) ) ;
#6932=VECTOR ( 'NONE', #3160, 1000.000000000000000 ) ;
#6939=DIRECTION ( 'NONE',  ( 1.000000000000000000, -0.000000000000000000, -0.000000000000000000 ) ) ;
#6940=VECTOR ( 'NONE', #9734, 1000.000000000000000 ) ;
#6941=DIRECTION ( 'NONE',  ( 1.000000000000000000, 0.000000000000000000, 0.000000000000000000 ) ) ;
#6942=VECTOR ( 'NONE', #4652, 1000.000000000000000 ) ;
#6946=VECTOR ( 'NONE', #2035, 1000.000000000000000 ) ;
#6947=EDGE_CURVE ( 'NONE', #7351, #4169, #6679, .T. ) ;
#6954=ADVANCED_FACE ( 'NONE', ( #329 ), #1124, .F. ) ;
#6955=CARTESIAN_POINT ( 'NONE',  ( 10.69739119071655686, 6.025400000000000311, -12.00000000000000000 ) ) ;
#6958=ORIENTED_EDGE ( 'NONE', *, *, #5191, .F. ) ;
#6960=LINE ( 'NONE', #7921, #5086 ) ;
#6976=ORIENTED_EDGE ( 'NONE', *, *, #1498, .T. ) ;
#6979=ORIENTED_EDGE ( 'NONE', *, *, #81, .T. ) ;
#6982=DIRECTION ( 'NONE',  ( -1.000000000000000000, 0.000000000000000000, -0.000000000000000000 ) ) ;
#6989=PLANE ( 'NONE',  #1354 ) ;
#6993=ADVANCED_FACE ( 'NONE', ( #283 ), #231, .T. ) ;
#6994=DIRECTION ( 'NONE',  ( -0.3420201433256627732, -0.9396926207859105373, 0.000000000000000000 ) ) ;
#7000=EDGE_LOOP ( 'NONE', ( #5593, #8062, #2140, #9378 ) ) ;
#7003=DIRECTION ( 'NONE',  ( 0.000000000000000000, -1.000000000000000000, 0.000000000000000000 ) ) ;
#7007=EDGE_LOOP ( 'NONE', ( #2158, #6807, #192, #1084, #2946, #9209, #9645, #1844, #5171, #4364, #4961, #3014 ) ) ;
#7009=VECTOR ( 'NONE', #7315, 1000.000000000000000 ) ;
#7013=EDGE_LOOP ( 'NONE', ( #827, #8045, #6008, #9859 ) ) ;
#7022=VERTEX_POINT ( 'NONE', #1976 ) ;
#7028=ORIENTED_EDGE ( 'NONE', *, *, #9938, .F. ) ;
#7031=ORIENTED_EDGE ( 'NONE', *, *, #9490, .T. ) ;
#7032=DIRECTION ( 'NONE',  ( 1.000000000000000000, -0.000000000000000000, -0.000000000000000000 ) ) ;
#7034=CARTESIAN_POINT ( 'NONE',  ( 16.98057649071655817, -10.02539999999999942, -12.00000000000000000 ) ) ;
#7037=ORIENTED_EDGE ( 'NONE', *, *, #8514, .T. ) ;
#7040=LINE ( 'NONE', #3807, #3120 ) ;
#7043=DIRECTION ( 'NONE',  ( 0.000000000000000000, 0.000000000000000000, 1.000000000000000000 ) ) ;
#7045=DIRECTION ( 'NONE',  ( 0.000000000000000000, 0.000000000000000000, -1.000000000000000000 ) ) ;
#7054=DIRECTION ( 'NONE',  ( 1.000000000000000000, -0.000000000000000000, -0.000000000000000000 ) ) ;
#7055=LINE ( 'NONE', #7861, #7467 ) ;
#7057=DIRECTION ( 'NONE',  ( 0.000000000000000000, 0.000000000000000000, -1.000000000000000000 ) ) ;
#7067=VERTEX_POINT ( 'NONE', #9393 ) ;
#7072=DIRECTION ( 'NONE',  ( 0.000000000000000000, -0.000000000000000000, 1.000000000000000000 ) ) ;
#7073=CARTESIAN_POINT ( 'NONE',  ( 0.000000000000000000, 3.750000000000000000, -12.00000000000000000 ) ) ;
#7077=EDGE_CURVE ( 'NONE', #4407, #1730, #8644, .T. ) ;
#7080=LINE ( 'NONE', #8844, #271 ) ;
#7082=FACE_OUTER_BOUND ( 'NONE', #593, .T. ) ;
#7085=DIRECTION ( 'NONE',  ( 0.000000000000000000, 0.000000000000000000, -1.000000000000000000 ) ) ;
#7090=CARTESIAN_POINT ( 'NONE',  ( 0.000000000000000000, 0.000000000000000000, 0.000000000000000000 ) ) ;
#7093=CARTESIAN_POINT ( 'NONE',  ( 8.980342580332745683, -7.750000000000000000, -12.00000000000000000 ) ) ;
#7104=LINE ( 'NONE', #641, #7842 ) ;
#7106=ORIENTED_EDGE ( 'NONE', *, *, #4867, .F. ) ;
#7107=EDGE_CURVE ( 'NONE', #5694, #5003, #584, .T. ) ;
#7114=VECTOR ( 'NONE', #3672, 1000.000000000000000 ) ;
#7115=EDGE_CURVE ( 'NONE', #3788, #8270, #10092, .T. ) ;
#7117=CARTESIAN_POINT ( 'NONE',  ( 20.12216914071655793, -10.02539999999999942, -12.00000000000000000 ) ) ;
#7128=ADVANCED_FACE ( 'NONE', ( #8494 ), #4606, .F. ) ;
#7129=LINE ( 'NONE', #7880, #9295 ) ;
#7130=CARTESIAN_POINT ( 'NONE',  ( 11.30300220323380600, 6.000000000000000000, -12.00000000000000000 ) ) ;
#7134=ORIENTED_EDGE ( 'NONE', *, *, #845, .F. ) ;
#7135=LINE ( 'NONE', #3963, #2467 ) ;
#7138=EDGE_CURVE ( 'NONE', #247, #2213, #3661, .T. ) ;
#7145=LINE ( 'NONE', #3757, #6661 ) ;
#7154=LINE ( 'NONE', #1550, #1164 ) ;
#7165=DIRECTION ( 'NONE',  ( 0.000000000000000000, 0.000000000000000000, -1.000000000000000000 ) ) ;
#7166=PLANE ( 'NONE',  #3404 ) ;
#7169=ADVANCED_FACE ( 'NONE', ( #1324 ), #6244, .F. ) ;
#7170=DIRECTION ( 'NONE',  ( 0.3420201433256627732, -0.9396926207859105373, 0.000000000000000000 ) ) ;
#7177=ORIENTED_EDGE ( 'NONE', *, *, #3704, .T. ) ;
#7179=LINE ( 'NONE', #10435, #9163 ) ;
#7183=DIRECTION ( 'NONE',  ( 0.000000000000000000, 0.000000000000000000, 1.000000000000000000 ) ) ;
#7186=CARTESIAN_POINT ( 'NONE',  ( 25.00000000000000000, -4.000000000000000000, -12.00000000000000000 ) ) ;
#7189=AXIS2_PLACEMENT_3D ( 'NONE', #4655, #10463, #6242 ) ;
#7190=EDGE_CURVE ( 'NONE', #10128, #307, #6143, .T. ) ;
#7195=VERTEX_POINT ( 'NONE', #5250 ) ;
#7200=VECTOR ( 'NONE', #5854, 1000.000000000000000 ) ;
#7209=VECTOR ( 'NONE', #5351, 1000.000000000000000 ) ;
#7212=CARTESIAN_POINT ( 'NONE',  ( 2.697157280332745266, 3.750000000000000000, -12.00000000000000000 ) ) ;
#7213=VECTOR ( 'NONE', #7382, 1000.000000000000000 ) ;
#7217=CARTESIAN_POINT ( 'NONE',  ( 23.26376179071655770, -10.02539999999999942, -12.00000000000000000 ) ) ;
#7220=CARTESIAN_POINT ( 'NONE',  ( 0.000000000000000000, 6.000000000000000000, -12.00000000000000000 ) ) ;
#7240=LINE ( 'NONE', #9795, #3386 ) ;
#7241=ORIENTED_EDGE ( 'NONE', *, *, #4537, .F. ) ;
#7243=ORIENTED_EDGE ( 'NONE', *, *, #8229, .T. ) ;
#7250=LINE ( 'NONE', #9599, #4465 ) ;
#7255=EDGE_LOOP ( 'NONE', ( #6454, #6617, #2110, #6370 ) ) ;
#7260=DIRECTION ( 'NONE',  ( 1.000000000000000000, -0.000000000000000000, -0.000000000000000000 ) ) ;
#7268=FACE_OUTER_BOUND ( 'NONE', #5657, .T. ) ;
#7273=DIRECTION ( 'NONE',  ( -0.3420201433256627732, 0.9396926207859105373, 0.000000000000000000 ) ) ;
#7274=VECTOR ( 'NONE', #8306, 1000.000000000000000 ) ;
#7275=CARTESIAN_POINT ( 'NONE',  ( 17.58618750323380908, 6.000000000000000000, -12.00000000000000000 ) ) ;
#7276=CARTESIAN_POINT ( 'NONE',  ( 0.000000000000000000, -4.000000000000000000, -12.00000000000000000 ) ) ;
#7278=ADVANCED_FACE ( 'NONE', ( #8909 ), #3130, .F. ) ;
#7279=CARTESIAN_POINT ( 'NONE',  ( 18.30309047890528618, 12.66178012940252451, 0.000000000000000000 ) ) ;
#7280=CARTESIAN_POINT ( 'NONE',  ( 14.44459485323380576, 6.000000000000000000, -12.00000000000000000 ) ) ;
#7282=UNCERTAINTY_MEASURE_WITH_UNIT (LENGTH_MEASURE( 1.000000000000000082E-05 ), #1906, 'distance_accuracy_value', 'NONE');
#7283=VECTOR ( 'NONE', #10243, 1000.000000000000000 ) ;
#7286=VERTEX_POINT ( 'NONE', #1649 ) ;
#7290=EDGE_LOOP ( 'NONE', ( #9174, #8611, #1811, #8924 ) ) ;
#7306=VERTEX_POINT ( 'NONE', #4822 ) ;
#7315=DIRECTION ( 'NONE',  ( -1.000000000000000000, 0.000000000000000000, -0.000000000000000000 ) ) ;
#7319=DIRECTION ( 'NONE',  ( 1.000000000000000000, 0.000000000000000000, 0.000000000000000000 ) ) ;
#7322=ORIENTED_EDGE ( 'NONE', *, *, #7743, .T. ) ;
#7328=CARTESIAN_POINT ( 'NONE',  ( 20.11292429676619520, 6.000000000000000000, -12.00000000000000000 ) ) ;
#7329=LINE ( 'NONE', #1661, #4498 ) ;
#7332=LINE ( 'NONE', #711, #7445 ) ;
#7337=VECTOR ( 'NONE', #8755, 1000.000000000000000 ) ;
#7344=AXIS2_PLACEMENT_3D ( 'NONE', #1068, #912, #2455 ) ;
#7347=CARTESIAN_POINT ( 'NONE',  ( 13.82973899676619745, -10.00000000000000000, 0.000000000000000000 ) ) ;
#7349=ORIENTED_EDGE ( 'NONE', *, *, #1183, .F. ) ;
#7351=VERTEX_POINT ( 'NONE', #1700 ) ;
#7357=DIRECTION ( 'NONE',  ( 0.000000000000000000, 0.000000000000000000, -1.000000000000000000 ) ) ;
#7358=ORIENTED_EDGE ( 'NONE', *, *, #3079, .F. ) ;
#7366=ORIENTED_EDGE ( 'NONE', *, *, #4881, .T. ) ;
#7370=DIRECTION ( 'NONE',  ( -0.000000000000000000, -0.000000000000000000, 1.000000000000000000 ) ) ;
#7374=ORIENTED_EDGE ( 'NONE', *, *, #36, .F. ) ;
#7375=LINE ( 'NONE', #5564, #9324 ) ;
#7382=DIRECTION ( 'NONE',  ( 0.3420201433256627732, -0.9396926207859105373, 0.000000000000000000 ) ) ;
#7389=EDGE_CURVE ( 'NONE', #1478, #3324, #7958, .T. ) ;
#7400=EDGE_CURVE ( 'NONE', #4726, #1894, #5559, .T. ) ;
#7406=DIRECTION ( 'NONE',  ( -0.000000000000000000, 1.000000000000000000, 0.000000000000000000 ) ) ;
#7411=VERTEX_POINT ( 'NONE', #1960 ) ;
#7413=CARTESIAN_POINT ( 'NONE',  ( 22.43558391966725907, -7.750000000000000000, 0.000000000000000000 ) ) ;
#7415=DIRECTION ( 'NONE',  ( -1.000000000000000000, 0.000000000000000000, -0.000000000000000000 ) ) ;
#7419=DIRECTION ( 'NONE',  ( 0.3420201433256627732, -0.9396926207859105373, 0.000000000000000000 ) ) ;
#7422=EDGE_LOOP ( 'NONE', ( #2474, #5795, #3086, #8325 ) ) ;
#7425=CARTESIAN_POINT ( 'NONE',  ( 4.404961046766194599, -10.00000000000000000, -12.00000000000000000 ) ) ;
#7444=CARTESIAN_POINT ( 'NONE',  ( 25.57717656966725883, -7.750000000000000000, 0.000000000000000000 ) ) ;
#7445=VECTOR ( 'NONE', #3252, 1000.000000000000000 ) ;
#7446=ADVANCED_FACE ( 'NONE', ( #3391 ), #316, .F. ) ;
#7449=AXIS2_PLACEMENT_3D ( 'NONE', #6448, #624, #6392 ) ;
#7451=CARTESIAN_POINT ( 'NONE',  ( 1.263368396766194612, 6.000000000000000000, -12.00000000000000000 ) ) ;
#7459=EDGE_CURVE ( 'NONE', #3241, #6828, #9923, .T. ) ;
#7461=VECTOR ( 'NONE', #1235, 1000.000000000000000 ) ;
#7467=VECTOR ( 'NONE', #8707, 1000.000000000000000 ) ;
#7473=ORIENTED_EDGE ( 'NONE', *, *, #6616, .F. ) ;
#7476=FACE_OUTER_BOUND ( 'NONE', #7973, .T. ) ;
#7477=EDGE_CURVE ( 'NONE', #9713, #1643, #1060, .T. ) ;
#7480=ORIENTED_EDGE ( 'NONE', *, *, #9463, .T. ) ;
#7484=ORIENTED_EDGE ( 'NONE', *, *, #1057, .F. ) ;
#7491=DIRECTION ( 'NONE',  ( 1.000000000000000000, 0.000000000000000000, 0.000000000000000000 ) ) ;
#7499=CARTESIAN_POINT ( 'NONE',  ( 16.98057649071655817, -10.02539999999999942, -12.00000000000000000 ) ) ;
#7509=EDGE_CURVE ( 'NONE', #10163, #244, #8277, .T. ) ;
#7513=AXIS2_PLACEMENT_3D ( 'NONE', #9444, #742, #7843 ) ;
#7521=ADVANCED_FACE ( 'NONE', ( #4282 ), #8224, .F. ) ;
#7523=LINE ( 'NONE', #9870, #6843 ) ;
#7526=LINE ( 'NONE', #8432, #1689 ) ;
#7529=ORIENTED_EDGE ( 'NONE', *, *, #6778, .F. ) ;
#7530=CARTESIAN_POINT ( 'NONE',  ( 5.019816903233806471, -10.00000000000000000, -12.00000000000000000 ) ) ;
#7533=ADVANCED_FACE ( 'NONE', ( #6565 ), #1909, .F. ) ;
#7534=LINE ( 'NONE', #9181, #1770 ) ;
#7535=CARTESIAN_POINT ( 'NONE',  ( 7.546553696766195252, 6.000000000000000000, -12.00000000000000000 ) ) ;
#7537=AXIS2_PLACEMENT_3D ( 'NONE', #5709, #4181, #8222 ) ;
#7541=CARTESIAN_POINT ( 'NONE',  ( 0.000000000000000000, 0.000000000000000000, -12.00000000000000000 ) ) ;
#7544=ADVANCED_FACE ( 'NONE', ( #2010 ), #5289, .F. ) ;
#7553=FACE_OUTER_BOUND ( 'NONE', #4696, .T. ) ;
#7570=ORIENTED_EDGE ( 'NONE', *, *, #9190, .F. ) ;
#7573=EDGE_LOOP ( 'NONE', ( #6310, #5597, #7938, #7615 ) ) ;
#7575=ADVANCED_FACE ( 'NONE', ( #4592 ), #3748, .F. ) ;
#7580=FACE_OUTER_BOUND ( 'NONE', #10101, .T. ) ;
#7582=LINE ( 'NONE', #8390, #2448 ) ;
#7586=DIRECTION ( 'NONE',  ( -0.000000000000000000, 1.000000000000000000, 0.000000000000000000 ) ) ;
#7594=VERTEX_POINT ( 'NONE', #369 ) ;
#7599=DIRECTION ( 'NONE',  ( 0.000000000000000000, -0.000000000000000000, 1.000000000000000000 ) ) ;
#7603=VECTOR ( 'NONE', #10212, 1000.000000000000000 ) ;
#7610=ORIENTED_EDGE ( 'NONE', *, *, #5201, .T. ) ;
#7615=ORIENTED_EDGE ( 'NONE', *, *, #8845, .T. ) ;
#7625=ORIENTED_EDGE ( 'NONE', *, *, #9970, .T. ) ;
#7627=DIRECTION ( 'NONE',  ( 0.000000000000000000, 0.000000000000000000, 1.000000000000000000 ) ) ;
#7628=CARTESIAN_POINT ( 'NONE',  ( 13.01080596966725622, 3.750000000000000000, -12.00000000000000000 ) ) ;
#7629=ORIENTED_EDGE ( 'NONE', *, *, #1437, .T. ) ;
#7631=VECTOR ( 'NONE', #9042, 1000.000000000000000 ) ;
#7641=LINE ( 'NONE', #379, #6495 ) ;
#7643=EDGE_CURVE ( 'NONE', #4426, #4307, #8430, .T. ) ;
#7647=CARTESIAN_POINT ( 'NONE',  ( 9.869213319667256457, -7.750000000000000000, -12.00000000000000000 ) ) ;
#7653=CARTESIAN_POINT ( 'NONE',  ( 2.697157280332745266, -7.750000000000000000, -12.00000000000000000 ) ) ;
#7664=EDGE_CURVE ( 'NONE', #717, #2729, #10130, .T. ) ;
#7666=ORIENTED_EDGE ( 'NONE', *, *, #996, .T. ) ;
#7669=AXIS2_PLACEMENT_3D ( 'NONE', #4813, #8849, #3070 ) ;
#7670=FACE_OUTER_BOUND ( 'NONE', #3127, .T. ) ;
#7671=EDGE_LOOP ( 'NONE', ( #10405, #9222, #5216, #9580 ) ) ;
#7678=EDGE_CURVE ( 'NONE', #2213, #6101, #6128, .T. ) ;
#7680=VECTOR ( 'NONE', #3137, 1000.000000000000000 ) ;
#7683=DIRECTION ( 'NONE',  ( 0.000000000000000000, 0.000000000000000000, 1.000000000000000000 ) ) ;
#7687=LINE ( 'NONE', #7034, #230 ) ;
#7692=CARTESIAN_POINT ( 'NONE',  ( 0.000000000000000000, -10.00000000000000000, 0.000000000000000000 ) ) ;
#7697=CARTESIAN_POINT ( 'NONE',  ( 0.000000000000000000, 0.000000000000000000, -12.00000000000000000 ) ) ;
#7698=DIRECTION ( 'NONE',  ( 0.3420201433256627732, 0.9396926207859105373, 0.000000000000000000 ) ) ;
#7699=CARTESIAN_POINT ( 'NONE',  ( 8.161409553233806236, -10.00000000000000000, -12.00000000000000000 ) ) ;
#7704=FACE_OUTER_BOUND ( 'NONE', #8094, .T. ) ;
#7709=DIRECTION ( 'NONE',  ( 0.000000000000000000, 1.000000000000000000, 0.000000000000000000 ) ) ;
#7712=ORIENTED_EDGE ( 'NONE', *, *, #9786, .F. ) ;
#7719=VECTOR ( 'NONE', #10196, 1000.000000000000000 ) ;
#7720=ORIENTED_EDGE ( 'NONE', *, *, #705, .F. ) ;
#7733=ORIENTED_EDGE ( 'NONE', *, *, #9463, .F. ) ;
#7734=CARTESIAN_POINT ( 'NONE',  ( 23.25451694676619496, -10.00000000000000000, -12.00000000000000000 ) ) ;
#7735=CARTESIAN_POINT ( 'NONE',  ( 13.01080596966725622, -7.750000000000000000, -12.00000000000000000 ) ) ;
#7738=DIRECTION ( 'NONE',  ( -1.000000000000000000, -0.000000000000000000, -0.000000000000000000 ) ) ;
#7739=CARTESIAN_POINT ( 'NONE',  ( 1.272613240716556016, 6.025400000000000311, -12.00000000000000000 ) ) ;
#7741=ORIENTED_EDGE ( 'NONE', *, *, #9955, .T. ) ;
#7743=EDGE_CURVE ( 'NONE', #1390, #9757, #5494, .T. ) ;
#7747=LINE ( 'NONE', #481, #9745 ) ;
#7757=LINE ( 'NONE', #6257, #3398 ) ;
#7760=DIRECTION ( 'NONE',  ( 0.000000000000000000, 1.000000000000000000, 0.000000000000000000 ) ) ;
#7763=ADVANCED_FACE ( 'NONE', ( #7082 ), #8735, .F. ) ;
#7764=CARTESIAN_POINT ( 'NONE',  ( 3.586028019667255595, 3.750000000000000000, 0.000000000000000000 ) ) ;
#7767=ORIENTED_EDGE ( 'NONE', *, *, #2816, .F. ) ;
#7778=FACE_OUTER_BOUND ( 'NONE', #1935, .T. ) ;
#7784=DIRECTION ( 'NONE',  ( 0.000000000000000000, 0.000000000000000000, -1.000000000000000000 ) ) ;
#7786=DIRECTION ( 'NONE',  ( 0.000000000000000000, 0.000000000000000000, -1.000000000000000000 ) ) ;
#7787=CARTESIAN_POINT ( 'NONE',  ( 0.000000000000000000, -10.00000000000000000, 0.000000000000000000 ) ) ;
#7799=LINE ( 'NONE', #8694, #7283 ) ;
#7802=CARTESIAN_POINT ( 'NONE',  ( 0.000000000000000000, 6.000000000000000000, -12.00000000000000000 ) ) ;
#7804=LINE ( 'NONE', #538, #8114 ) ;
#7814=LINE ( 'NONE', #1444, #8143 ) ;
#7816=CARTESIAN_POINT ( 'NONE',  ( 8.980342580332745683, 3.750000000000000000, 0.000000000000000000 ) ) ;
#7821=CARTESIAN_POINT ( 'NONE',  ( 20.71853530928344611, 6.025400000000000311, -12.00000000000000000 ) ) ;
#7824=VERTEX_POINT ( 'NONE', #3854 ) ;
#7828=ORIENTED_EDGE ( 'NONE', *, *, #7664, .T. ) ;
#7830=DIRECTION ( 'NONE',  ( 0.000000000000000000, -0.000000000000000000, 1.000000000000000000 ) ) ;
#7831=ORIENTED_EDGE ( 'NONE', *, *, #2671, .T. ) ;
#7841=EDGE_CURVE ( 'NONE', #9951, #4800, #5652, .T. ) ;
#7842=VECTOR ( 'NONE', #2186, 1000.000000000000000 ) ;
#7843=DIRECTION ( 'NONE',  ( 0.000000000000000000, 0.000000000000000000, -1.000000000000000000 ) ) ;
#7846=CARTESIAN_POINT ( 'NONE',  ( 5.010572059283444624, 6.025400000000000311, -12.00000000000000000 ) ) ;
#7850=DIRECTION ( 'NONE',  ( 0.000000000000000000, 0.000000000000000000, 1.000000000000000000 ) ) ;
#7857=CARTESIAN_POINT ( 'NONE',  ( 0.000000000000000000, 6.000000000000000000, -12.00000000000000000 ) ) ;
#7858=EDGE_LOOP ( 'NONE', ( #2648, #9072, #1467, #5430, #5345, #2166, #7106, #5189, #4631, #6294, #1634, #3207, #5242, #2956, #5650, #5019, #197, #7666, #10012, #8794, #6069, #7610, #9601, #3985, #7134, #9697, #7733, #7241, #4626, #1308, #8163, #2262, #8177, #2805, #5939, #7925 ) ) ;
#7861=CARTESIAN_POINT ( 'NONE',  ( 12.75489823682933554, 10.64240329930025375, 0.000000000000000000 ) ) ;
#7863=MECHANICAL_DESIGN_GEOMETRIC_PRESENTATION_REPRESENTATION('',(#2114),#4818);
#7868=CARTESIAN_POINT ( 'NONE',  ( 23.86937280323380506, -10.00000000000000000, -12.00000000000000000 ) ) ;
#7869=VECTOR ( 'NONE', #3193, 1000.000000000000000 ) ;
#7873=ORIENTED_EDGE ( 'NONE', *, *, #8272, .F. ) ;
#7880=CARTESIAN_POINT ( 'NONE',  ( 3.586028019667255595, -7.750000000000000000, 0.000000000000000000 ) ) ;
#7887=VECTOR ( 'NONE', #6527, 1000.000000000000000 ) ;
#7896=ORIENTED_EDGE ( 'NONE', *, *, #5956, .F. ) ;
#7897=AXIS2_PLACEMENT_3D ( 'NONE', #7802, #3080, #5352 ) ;
#7901=DIRECTION ( 'NONE',  ( -1.000000000000000000, 0.000000000000000000, 0.000000000000000000 ) ) ;
#7903=ADVANCED_FACE ( 'NONE', ( #8211 ), #1897, .F. ) ;
#7905=CARTESIAN_POINT ( 'NONE',  ( 3.586028019667255595, 3.750000000000000000, -12.00000000000000000 ) ) ;
#7914=DIRECTION ( 'NONE',  ( 0.3420201433256627732, -0.9396926207859105373, 0.000000000000000000 ) ) ;
#7916=DIRECTION ( 'NONE',  ( 0.000000000000000000, 1.000000000000000000, 0.000000000000000000 ) ) ;
#7918=LINE ( 'NONE', #6472, #7887 ) ;
#7919=FACE_OUTER_BOUND ( 'NONE', #658, .T. ) ;
#7921=CARTESIAN_POINT ( 'NONE',  ( 10.69739119071655686, 6.025400000000000311, -12.00000000000000000 ) ) ;
#7925=ORIENTED_EDGE ( 'NONE', *, *, #3902, .F. ) ;
#7929=CARTESIAN_POINT ( 'NONE',  ( 3.586028019667255595, 3.750000000000000000, -12.00000000000000000 ) ) ;
#7933=ORIENTED_EDGE ( 'NONE', *, *, #7107, .T. ) ;
#7934=CARTESIAN_POINT ( 'NONE',  ( 0.000000000000000000, 3.750000000000000000, -12.00000000000000000 ) ) ;
#7937=EDGE_CURVE ( 'NONE', #3241, #10315, #3529, .T. ) ;
#7938=ORIENTED_EDGE ( 'NONE', *, *, #5582, .T. ) ;
#7939=CARTESIAN_POINT ( 'NONE',  ( 13.01080596966725622, 3.750000000000000000, 0.000000000000000000 ) ) ;
#7941=DIRECTION ( 'NONE',  ( -1.000000000000000000, -0.000000000000000000, -0.000000000000000000 ) ) ;
#7942=VERTEX_POINT ( 'NONE', #1687 ) ;
#7944=CARTESIAN_POINT ( 'NONE',  ( 0.000000000000000000, -4.000000000000000000, 0.000000000000000000 ) ) ;
#7948=VECTOR ( 'NONE', #8561, 1000.000000000000000 ) ;
#7952=MANIFOLD_SOLID_BREP ( 'Extrude-Thin1', #431 ) ;
#7953=EDGE_LOOP ( 'NONE', ( #9765, #2837, #10489, #9165 ) ) ;
#7958=LINE ( 'NONE', #6460, #3886 ) ;
#7961=DIRECTION ( 'NONE',  ( 0.000000000000000000, -1.000000000000000000, -0.000000000000000000 ) ) ;
#7967=COLOUR_RGB ( '', 0.66274510, 0.83137255, 0.94901961) ;
#7971=DIRECTION ( 'NONE',  ( 0.000000000000000000, 0.000000000000000000, -1.000000000000000000 ) ) ;
#7973=EDGE_LOOP ( 'NONE', ( #9707, #7873, #1045, #4575 ) ) ;
#7976=VECTOR ( 'NONE', #8505, 1000.000000000000000 ) ;
#7998=ORIENTED_EDGE ( 'NONE', *, *, #1022, .T. ) ;
#7999=VERTEX_POINT ( 'NONE', #2686 ) ;
#8004=CARTESIAN_POINT ( 'NONE',  ( 16.97133164676619899, 6.000000000000000000, -12.00000000000000000 ) ) ;
#8007=EDGE_CURVE ( 'NONE', #10490, #4313, #6911, .T. ) ;
#8009=DIRECTION ( 'NONE',  ( 0.000000000000000000, 0.000000000000000000, 1.000000000000000000 ) ) ;
#8013=DIRECTION ( 'NONE',  ( 1.000000000000000000, 0.000000000000000000, 0.000000000000000000 ) ) ;
#8019=ORIENTED_EDGE ( 'NONE', *, *, #8874, .T. ) ;
#8026=DIRECTION ( 'NONE',  ( 0.000000000000000000, 0.000000000000000000, 1.000000000000000000 ) ) ;
#8032=DIRECTION ( 'NONE',  ( 0.3420201433256627732, 0.9396926207859105373, -0.000000000000000000 ) ) ;
#8033=LINE ( 'NONE', #10483, #8963 ) ;
#8034=CARTESIAN_POINT ( 'NONE',  ( 6.727620669667255804, 3.750000000000000000, -12.00000000000000000 ) ) ;
#8037=UNCERTAINTY_MEASURE_WITH_UNIT (LENGTH_MEASURE( 1.000000000000000082E-05 ), #5811, 'distance_accuracy_value', 'NONE');
#8044=EDGE_CURVE ( 'NONE', #3477, #7306, #3633, .T. ) ;
#8045=ORIENTED_EDGE ( 'NONE', *, *, #7509, .T. ) ;
#8046=CARTESIAN_POINT ( 'NONE',  ( 23.26376179071655770, 6.025400000000000311, -12.00000000000000000 ) ) ;
#8047=CARTESIAN_POINT ( 'NONE',  ( 0.4444353696672553311, -7.750000000000000000, -12.00000000000000000 ) ) ;
#8048=ORIENTED_EDGE ( 'NONE', *, *, #8095, .T. ) ;
#8062=ORIENTED_EDGE ( 'NONE', *, *, #5631, .F. ) ;
#8065=VERTEX_POINT ( 'NONE', #6169 ) ;
#8075=CARTESIAN_POINT ( 'NONE',  ( 23.86937280323380506, 6.000000000000001776, 0.000000000000000000 ) ) ;
#8079=EDGE_CURVE ( 'NONE', #6457, #4313, #6056, .T. ) ;
#8080=FACE_OUTER_BOUND ( 'NONE', #6907, .T. ) ;
#8081=LINE ( 'NONE', #4143, #6002 ) ;
#8082=LINE ( 'NONE', #812, #7213 ) ;
#8083=CARTESIAN_POINT ( 'NONE',  ( 23.86012795928344588, 6.025400000000000311, -12.00000000000000000 ) ) ;
#8091=LINE ( 'NONE', #6588, #1554 ) ;
#8092=LINE ( 'NONE', #10381, #2391 ) ;
#8094=EDGE_LOOP ( 'NONE', ( #3220, #7831, #1684, #2553 ) ) ;
#8095=EDGE_CURVE ( 'NONE', #4888, #2377, #2103, .T. ) ;
#8104=CARTESIAN_POINT ( 'NONE',  ( 0.000000000000000000, -10.00000000000000000, -12.00000000000000000 ) ) ;
#8110=ORIENTED_EDGE ( 'NONE', *, *, #36, .T. ) ;
#8114=VECTOR ( 'NONE', #6994, 1000.000000000000000 ) ;
#8115=ORIENTED_EDGE ( 'NONE', *, *, #4588, .F. ) ;
#8125=ADVANCED_FACE ( 'NONE', ( #7670 ), #4527, .F. ) ;
#8128=CARTESIAN_POINT ( 'NONE',  ( 22.43558391966725907, 3.750000000000000000, -12.00000000000000000 ) ) ;
#8130=LINE ( 'NONE', #866, #865 ) ;
#8131=VECTOR ( 'NONE', #1547, 1000.000000000000000 ) ;
#8143=VECTOR ( 'NONE', #8705, 1000.000000000000000 ) ;
#8146=ORIENTED_EDGE ( 'NONE', *, *, #6334, .T. ) ;
#8150=ORIENTED_EDGE ( 'NONE', *, *, #628, .T. ) ;
#8158=ORIENTED_EDGE ( 'NONE', *, *, #10433, .T. ) ;
#8159=VERTEX_POINT ( 'NONE', #504 ) ;
#8161=LINE ( 'NONE', #8210, #9926 ) ;
#8163=ORIENTED_EDGE ( 'NONE', *, *, #387, .F. ) ;
#8165=PLANE ( 'NONE',  #7669 ) ;
#8170=PLANE ( 'NONE',  #2286 ) ;
#8177=ORIENTED_EDGE ( 'NONE', *, *, #4450, .T. ) ;
#8193=VECTOR ( 'NONE', #9893, 1000.000000000000000 ) ;
#8195=EDGE_LOOP ( 'NONE', ( #9205, #2, #3397, #8902 ) ) ;
#8204=ORIENTED_EDGE ( 'NONE', *, *, #4946, .T. ) ;
#8209=ORIENTED_EDGE ( 'NONE', *, *, #1171, .T. ) ;
#8210=CARTESIAN_POINT ( 'NONE',  ( 0.000000000000000000, 0.000000000000000000, -12.00000000000000000 ) ) ;
#8211=FACE_OUTER_BOUND ( 'NONE', #5175, .T. ) ;
#8215=( GEOMETRIC_REPRESENTATION_CONTEXT ( 3 ) GLOBAL_UNCERTAINTY_ASSIGNED_CONTEXT ( ( #8037 ) ) GLOBAL_UNIT_ASSIGNED_CONTEXT ( ( #5811, #5962, #4278 ) ) REPRESENTATION_CONTEXT ( 'NONE', 'WORKASPACE' ) );
#8217=ORIENTED_EDGE ( 'NONE', *, *, #6947, .T. ) ;
#8222=DIRECTION ( 'NONE',  ( 0.3420201433256627732, -0.9396926207859105373, 0.000000000000000000 ) ) ;
#8224=PLANE ( 'NONE',  #9665 ) ;
#8225=VERTEX_POINT ( 'NONE', #613 ) ;
#8226=FACE_OUTER_BOUND ( 'NONE', #5551, .T. ) ;
#8229=EDGE_CURVE ( 'NONE', #789, #7999, #10437, .T. ) ;
#8231=ORIENTED_EDGE ( 'NONE', *, *, #9938, .T. ) ;
#8247=EDGE_CURVE ( 'NONE', #909, #8622, #1574, .T. ) ;
#8248=DIRECTION ( 'NONE',  ( -0.000000000000000000, -1.000000000000000000, -0.000000000000000000 ) ) ;
#8252=FACE_OUTER_BOUND ( 'NONE', #9489, .T. ) ;
#8254=ORIENTED_EDGE ( 'NONE', *, *, #7743, .F. ) ;
#8265=( NAMED_UNIT ( * ) PLANE_ANGLE_UNIT ( ) SI_UNIT ( $, .RADIAN. ) );
#8270=VERTEX_POINT ( 'NONE', #7929 ) ;
#8272=EDGE_CURVE ( 'NONE', #7306, #2835, #8092, .T. ) ;
#8274=VERTEX_POINT ( 'NONE', #6325 ) ;
#8277=LINE ( 'NONE', #9117, #6246 ) ;
#8283=CARTESIAN_POINT ( 'NONE',  ( 16.98057649071655817, 6.025400000000000311, 0.000000000000000000 ) ) ;
#8289=DIRECTION ( 'NONE',  ( 0.000000000000000000, 0.000000000000000000, 1.000000000000000000 ) ) ;
#8300=DIRECTION ( 'NONE',  ( 0.000000000000000000, 0.000000000000000000, -1.000000000000000000 ) ) ;
#8301=CARTESIAN_POINT ( 'NONE',  ( 1.263368396766194612, -10.00000000000000000, -12.00000000000000000 ) ) ;
#8305=LINE ( 'NONE', #1036, #6068 ) ;
#8306=DIRECTION ( 'NONE',  ( -0.3420201433256627732, 0.9396926207859105373, 0.000000000000000000 ) ) ;
#8319=ADVANCED_FACE ( 'NONE', ( #1672 ), #5052, .F. ) ;
#8325=ORIENTED_EDGE ( 'NONE', *, *, #4279, .F. ) ;
#8326=AXIS2_PLACEMENT_3D ( 'NONE', #979, #1034, #2675 ) ;
#8328=PRESENTATION_STYLE_ASSIGNMENT (( #5075 ) ) ;
#8333=VERTEX_POINT ( 'NONE', #8301 ) ;
#8334=EDGE_CURVE ( 'NONE', #10028, #6306, #2473, .T. ) ;
#8341=FACE_OUTER_BOUND ( 'NONE', #2479, .T. ) ;
#8348=DIRECTION ( 'NONE',  ( 0.000000000000000000, 0.000000000000000000, -1.000000000000000000 ) ) ;
#8356=LINE ( 'NONE', #5110, #2024 ) ;
#8358=DIRECTION ( 'NONE',  ( 0.000000000000000000, 0.000000000000000000, 1.000000000000000000 ) ) ;
#8367=ORIENTED_EDGE ( 'NONE', *, *, #6786, .F. ) ;
#8373=VECTOR ( 'NONE', #6085, 1000.000000000000000 ) ;
#8380=CARTESIAN_POINT ( 'NONE',  ( 12.12193523033274545, 3.750000000000000000, -12.00000000000000000 ) ) ;
#8389=EDGE_CURVE ( 'NONE', #138, #1592, #930, .T. ) ;
#8390=CARTESIAN_POINT ( 'NONE',  ( 10.68814634676619413, -10.00000000000000000, -12.00000000000000000 ) ) ;
#8395=CARTESIAN_POINT ( 'NONE',  ( 22.43558391966725907, 3.750000000000000000, 0.000000000000000000 ) ) ;
#8414=ORIENTED_EDGE ( 'NONE', *, *, #9786, .T. ) ;
#8418=LINE ( 'NONE', #10063, #9236 ) ;
#8430=LINE ( 'NONE', #7735, #2704 ) ;
#8432=CARTESIAN_POINT ( 'NONE',  ( 21.54671318033274829, 3.750000000000000000, -12.00000000000000000 ) ) ;
#8436=ORIENTED_EDGE ( 'NONE', *, *, #4165, .F. ) ;
#8437=CARTESIAN_POINT ( 'NONE',  ( 21.54671318033274829, 3.750000000000000000, -12.00000000000000000 ) ) ;
#8443=FACE_OUTER_BOUND ( 'NONE', #2845, .T. ) ;
#8453=CARTESIAN_POINT ( 'NONE',  ( 20.11292429676619520, -10.00000000000000000, -12.00000000000000000 ) ) ;
#8455=EDGE_CURVE ( 'NONE', #6381, #2302, #2575, .T. ) ;
#8463=VECTOR ( 'NONE', #4997, 1000.000000000000000 ) ;
#8466=CARTESIAN_POINT ( 'NONE',  ( 14.43535000928344481, 6.025400000000000311, -12.00000000000000000 ) ) ;
#8468=CARTESIAN_POINT ( 'NONE',  ( 25.57717656966725883, 3.750000000000000000, -12.00000000000000000 ) ) ;
#8477=AXIS2_PLACEMENT_3D ( 'NONE', #7846, #8802, #535 ) ;
#8478=EDGE_LOOP ( 'NONE', ( #1988, #9920, #6276, #6057 ) ) ;
#8481=ORIENTED_EDGE ( 'NONE', *, *, #2159, .F. ) ;
#8483=VECTOR ( 'NONE', #5207, 1000.000000000000000 ) ;
#8484=DIRECTION ( 'NONE',  ( -0.000000000000000000, 1.000000000000000000, 0.000000000000000000 ) ) ;
#8488=CARTESIAN_POINT ( 'NONE',  ( 13.01080596966725622, 3.750000000000000000, -12.00000000000000000 ) ) ;
#8489=CARTESIAN_POINT ( 'NONE',  ( 4.414205890716556446, -10.02539999999999942, -12.00000000000000000 ) ) ;
#8493=EDGE_CURVE ( 'NONE', #1396, #4686, #8507, .T. ) ;
#8494=FACE_OUTER_BOUND ( 'NONE', #8929, .T. ) ;
#8503=DIRECTION ( 'NONE',  ( -1.000000000000000000, 0.000000000000000000, -0.000000000000000000 ) ) ;
#8505=DIRECTION ( 'NONE',  ( 0.3420201433256627732, 0.9396926207859105373, -0.000000000000000000 ) ) ;
#8506=CARTESIAN_POINT ( 'NONE',  ( 20.12216914071655793, 6.025400000000000311, 0.000000000000000000 ) ) ;
#8507=LINE ( 'NONE', #394, #9685 ) ;
#8510=LINE ( 'NONE', #7868, #9156 ) ;
#8514=EDGE_CURVE ( 'NONE', #2835, #6209, #1135, .T. ) ;
#8525=ORIENTED_EDGE ( 'NONE', *, *, #4736, .T. ) ;
#8531=DIRECTION ( 'NONE',  ( 0.000000000000000000, 0.000000000000000000, -1.000000000000000000 ) ) ;
#8532=ORIENTED_EDGE ( 'NONE', *, *, #1767, .T. ) ;
#8533=LINE ( 'NONE', #372, #3038 ) ;
#8534=CARTESIAN_POINT ( 'NONE',  ( 18.40512053033274853, 3.750000000000000000, 0.000000000000000000 ) ) ;
#8535=LINE ( 'NONE', #3057, #6409 ) ;
#8543=DIRECTION ( 'NONE',  ( 1.000000000000000000, -0.000000000000000000, -0.000000000000000000 ) ) ;
#8544=ADVANCED_FACE ( 'NONE', ( #10053 ), #4463, .T. ) ;
#8546=CARTESIAN_POINT ( 'NONE',  ( 1.272613240716556016, -10.02539999999999942, -12.00000000000000000 ) ) ;
#8552=DIRECTION ( 'NONE',  ( 0.3420201433256627732, 0.9396926207859105373, 0.000000000000000000 ) ) ;
#8553=VECTOR ( 'NONE', #9972, 1000.000000000000000 ) ;
#8555=CARTESIAN_POINT ( 'NONE',  ( 13.01080596966725622, -7.750000000000000000, 0.000000000000000000 ) ) ;
#8558=DIRECTION ( 'NONE',  ( -1.000000000000000000, 0.000000000000000000, -0.000000000000000000 ) ) ;
#8561=DIRECTION ( 'NONE',  ( 0.3420201433256627732, 0.9396926207859105373, -0.000000000000000000 ) ) ;
#8571=DIRECTION ( 'NONE',  ( -0.9396926207859105373, -0.3420201433256627732, 0.000000000000000000 ) ) ;
#8576=EDGE_CURVE ( 'NONE', #3392, #9203, #345, .T. ) ;
#8578=CARTESIAN_POINT ( 'NONE',  ( -0.000000000000000000, -4.000000000000000000, -10.00000000000000000 ) ) ;
#8584=CARTESIAN_POINT ( 'NONE',  ( 0.000000000000000000, -4.000000000000000000, -12.00000000000000000 ) ) ;
#8590=CARTESIAN_POINT ( 'NONE',  ( 17.58618750323380553, -10.00000000000000000, -12.00000000000000000 ) ) ;
#8601=CARTESIAN_POINT ( 'NONE',  ( 0.000000000000000000, -10.00000000000000000, -12.00000000000000000 ) ) ;
#8602=LINE ( 'NONE', #5414, #3736 ) ;
#8611=ORIENTED_EDGE ( 'NONE', *, *, #5956, .T. ) ;
#8615=ORIENTED_EDGE ( 'NONE', *, *, #3136, .T. ) ;
#8621=DIRECTION ( 'NONE',  ( 0.9396926207859105373, 0.3420201433256627732, 0.000000000000000000 ) ) ;
#8622=VERTEX_POINT ( 'NONE', #10209 ) ;
#8623=VECTOR ( 'NONE', #10181, 1000.000000000000000 ) ;
#8625=ADVANCED_FACE ( 'NONE', ( #1083 ), #4413, .T. ) ;
#8626=DIRECTION ( 'NONE',  ( -1.000000000000000000, -0.000000000000000000, -0.000000000000000000 ) ) ;
#8628=ADVANCED_FACE ( 'NONE', ( #2938 ), #10104, .F. ) ;
#8639=LINE ( 'NONE', #3809, #4806 ) ;
#8640=ADVANCED_FACE ( 'NONE', ( #7553 ), #295, .F. ) ;
#8642=AXIS2_PLACEMENT_3D ( 'NONE', #9158, #7406, #7357 ) ;
#8644=LINE ( 'NONE', #1278, #10269 ) ;
#8651=VECTOR ( 'NONE', #9871, 1000.000000000000000 ) ;
#8652=AXIS2_PLACEMENT_3D ( 'NONE', #3519, #6740, #2728 ) ;
#8654=DIRECTION ( 'NONE',  ( 0.000000000000000000, -0.000000000000000000, 1.000000000000000000 ) ) ;
#8658=AXIS2_PLACEMENT_3D ( 'NONE', #7499, #242, #2574 ) ;
#8659=FACE_OUTER_BOUND ( 'NONE', #7573, .T. ) ;
#8660=DIRECTION ( 'NONE',  ( 0.000000000000000000, -1.000000000000000000, -0.000000000000000000 ) ) ;
#8662=ORIENTED_EDGE ( 'NONE', *, *, #7190, .F. ) ;
#8674=ORIENTED_EDGE ( 'NONE', *, *, #4254, .F. ) ;
#8681=PLANE ( 'NONE',  #4314 ) ;
#8684=CARTESIAN_POINT ( 'NONE',  ( 16.15239861966725599, -7.750000000000000000, -12.00000000000000000 ) ) ;
#8685=CARTESIAN_POINT ( 'NONE',  ( 3.586028019667255595, -7.750000000000000000, -12.00000000000000000 ) ) ;
#8687=ORIENTED_EDGE ( 'NONE', *, *, #297, .T. ) ;
#8690=ADVANCED_FACE ( 'NONE', ( #8764 ), #5525, .F. ) ;
#8694=CARTESIAN_POINT ( 'NONE',  ( 0.000000000000000000, -4.000000000000000000, 0.000000000000000000 ) ) ;
#8705=DIRECTION ( 'NONE',  ( -1.000000000000000000, -0.000000000000000000, -0.000000000000000000 ) ) ;
#8706=CARTESIAN_POINT ( 'NONE',  ( 23.86012795928344588, -10.02539999999999942, -12.00000000000000000 ) ) ;
#8707=DIRECTION ( 'NONE',  ( -0.3420201433256627732, 0.9396926207859105373, 0.000000000000000000 ) ) ;
#8708=CARTESIAN_POINT ( 'NONE',  ( 0.000000000000000000, 3.750000000000000000, 0.000000000000000000 ) ) ;
#8709=CARTESIAN_POINT ( 'NONE',  ( 0.4444353696672553311, 3.750000000000000000, -12.00000000000000000 ) ) ;
#8714=APPLICATION_CONTEXT ( 'automotive_design' ) ;
#8721=ORIENTED_EDGE ( 'NONE', *, *, #7115, .F. ) ;
#8727=DIRECTION ( 'NONE',  ( 0.000000000000000000, 0.000000000000000000, -1.000000000000000000 ) ) ;
#8730=VERTEX_POINT ( 'NONE', #9682 ) ;
#8731=EDGE_CURVE ( 'NONE', #6440, #1730, #4566, .T. ) ;
#8732=VECTOR ( 'NONE', #6941, 1000.000000000000000 ) ;
#8734=DIRECTION ( 'NONE',  ( 0.9396926207859105373, 0.3420201433256627732, 0.000000000000000000 ) ) ;
#8735=PLANE ( 'NONE',  #7449 ) ;
#8736=ORIENTED_EDGE ( 'NONE', *, *, #6395, .T. ) ;
#8737=DIRECTION ( 'NONE',  ( 0.000000000000000000, 0.000000000000000000, 1.000000000000000000 ) ) ;
#8738=EDGE_CURVE ( 'NONE', #614, #3582, #2193, .T. ) ;
#8751=LINE ( 'NONE', #62, #2525 ) ;
#8755=DIRECTION ( 'NONE',  ( -0.000000000000000000, -0.000000000000000000, 1.000000000000000000 ) ) ;
#8763=EDGE_CURVE ( 'NONE', #5526, #4582, #1563, .T. ) ;
#8764=FACE_OUTER_BOUND ( 'NONE', #2576, .T. ) ;
#8768=DIRECTION ( 'NONE',  ( 0.000000000000000000, 1.000000000000000000, 0.000000000000000000 ) ) ;
#8773=ADVANCED_FACE ( 'NONE', ( #7919 ), #7166, .F. ) ;
#8774=CARTESIAN_POINT ( 'NONE',  ( 5.019816903233805583, -10.00000000000000000, -12.00000000000000000 ) ) ;
#8783=ORIENTED_EDGE ( 'NONE', *, *, #4911, .F. ) ;
#8786=LINE ( 'NONE', #3217, #5500 ) ;
#8794=ORIENTED_EDGE ( 'NONE', *, *, #10301, .F. ) ;
#8797=DIRECTION ( 'NONE',  ( 0.000000000000000000, 0.000000000000000000, -1.000000000000000000 ) ) ;
#8799=VECTOR ( 'NONE', #8737, 1000.000000000000000 ) ;
#8800=ORIENTED_EDGE ( 'NONE', *, *, #10327, .F. ) ;
#8802=DIRECTION ( 'NONE',  ( -0.9396926207859105373, -0.3420201433256627732, 0.000000000000000000 ) ) ;
#8803=CARTESIAN_POINT ( 'NONE',  ( 23.25451694676619496, 6.000000000000000000, -12.00000000000000000 ) ) ;
#8811=DIRECTION ( 'NONE',  ( -0.9396926207859105373, -0.3420201433256627732, 0.000000000000000000 ) ) ;
#8814=ORIENTED_EDGE ( 'NONE', *, *, #5631, .T. ) ;
#8816=VECTOR ( 'NONE', #3035, 1000.000000000000000 ) ;
#8818=AXIS2_PLACEMENT_3D ( 'NONE', #6719, #377, #3602 ) ;
#8819=DIRECTION ( 'NONE',  ( -1.000000000000000000, -0.000000000000000000, -0.000000000000000000 ) ) ;
#8823=VECTOR ( 'NONE', #8013, 1000.000000000000000 ) ;
#8826=VECTOR ( 'NONE', #9518, 1000.000000000000000 ) ;
#8839=CARTESIAN_POINT ( 'NONE',  ( 23.25451694676619496, -10.00000000000000000, 0.000000000000000000 ) ) ;
#8844=CARTESIAN_POINT ( 'NONE',  ( 25.00000000000000000, -4.000000000000000000, -12.00000000000000000 ) ) ;
#8845=EDGE_CURVE ( 'NONE', #6101, #9404, #2755, .T. ) ;
#8849=DIRECTION ( 'NONE',  ( 0.000000000000000000, 1.000000000000000000, 0.000000000000000000 ) ) ;
#8853=EDGE_LOOP ( 'NONE', ( #2676, #9894, #2747, #6958 ) ) ;
#8857=LINE ( 'NONE', #114, #4168 ) ;
#8862=ORIENTED_EDGE ( 'NONE', *, *, #9552, .T. ) ;
#8866=DIRECTION ( 'NONE',  ( 0.000000000000000000, 1.000000000000000000, 0.000000000000000000 ) ) ;
#8872=FACE_OUTER_BOUND ( 'NONE', #3585, .T. ) ;
#8873=DIRECTION ( 'NONE',  ( 0.3420201433256627732, 0.9396926207859105373, 0.000000000000000000 ) ) ;
#8874=EDGE_CURVE ( 'NONE', #3324, #9213, #1662, .T. ) ;
#8875=LINE ( 'NONE', #1615, #2052 ) ;
#8876=CARTESIAN_POINT ( 'NONE',  ( 19.29399126966725575, 3.750000000000000000, -12.00000000000000000 ) ) ;
#8877=VECTOR ( 'NONE', #4192, 1000.000000000000000 ) ;
#8885=ORIENTED_EDGE ( 'NONE', *, *, #552, .F. ) ;
#8887=EDGE_CURVE ( 'NONE', #8915, #2276, #4837, .T. ) ;
#8890=COLOUR_RGB ( '', 0.66274510, 0.83137255, 0.94901961) ;
#8896=ORIENTED_EDGE ( 'NONE', *, *, #6802, .F. ) ;
#8899=ADVANCED_FACE ( 'NONE', ( #3251 ), #4943, .F. ) ;
#8902=ORIENTED_EDGE ( 'NONE', *, *, #4810, .F. ) ;
#8909=FACE_OUTER_BOUND ( 'NONE', #7000, .T. ) ;
#8910=ADVANCED_FACE ( 'NONE', ( #9030 ), #1718, .F. ) ;
#8915=VERTEX_POINT ( 'NONE', #5627 ) ;
#8921=CARTESIAN_POINT ( 'NONE',  ( 5.019816903233805583, 6.000000000000000000, -12.00000000000000000 ) ) ;
#8923=CARTESIAN_POINT ( 'NONE',  ( 10.69739119071655686, 6.025400000000000311, 0.000000000000000000 ) ) ;
#8924=ORIENTED_EDGE ( 'NONE', *, *, #7841, .F. ) ;
#8929=EDGE_LOOP ( 'NONE', ( #204, #7629, #390, #752 ) ) ;
#8930=VERTEX_POINT ( 'NONE', #6771 ) ;
#8931=PLANE ( 'NONE',  #8658 ) ;
#8941=ADVANCED_FACE ( 'NONE', ( #8872 ), #126, .F. ) ;
#8943=CARTESIAN_POINT ( 'NONE',  ( 11.29375735928344504, 6.025400000000000311, -12.00000000000000000 ) ) ;
#8947=CARTESIAN_POINT ( 'NONE',  ( 0.000000000000000000, -10.00000000000000000, 0.000000000000000000 ) ) ;
#8949=ORIENTED_EDGE ( 'NONE', *, *, #9551, .F. ) ;
#8956=CARTESIAN_POINT ( 'NONE',  ( 1.263368396766194612, 6.000000000000000000, 0.000000000000000000 ) ) ;
#8963=VECTOR ( 'NONE', #3253, 1000.000000000000000 ) ;
#8969=VECTOR ( 'NONE', #10424, 1000.000000000000000 ) ;
#8993=DIRECTION ( 'NONE',  ( 0.000000000000000000, 0.000000000000000000, 1.000000000000000000 ) ) ;
#8994=ORIENTED_EDGE ( 'NONE', *, *, #6003, .T. ) ;
#9002=FILL_AREA_STYLE ('',( #100 ) ) ;
#9012=DIRECTION ( 'NONE',  ( 0.000000000000000000, 0.000000000000000000, -1.000000000000000000 ) ) ;
#9014=DIRECTION ( 'NONE',  ( -0.9396926207859105373, 0.3420201433256627732, 0.000000000000000000 ) ) ;
#9019=EDGE_CURVE ( 'NONE', #4895, #6012, #7687, .T. ) ;
#9022=CARTESIAN_POINT ( 'NONE',  ( 13.01080596966725622, -7.750000000000000000, 0.000000000000000000 ) ) ;
#9030=FACE_OUTER_BOUND ( 'NONE', #3673, .T. ) ;
#9033=EDGE_CURVE ( 'NONE', #9713, #7594, #4494, .T. ) ;
#9041=DIRECTION ( 'NONE',  ( 0.9396926207859105373, 0.3420201433256627732, 0.000000000000000000 ) ) ;
#9042=DIRECTION ( 'NONE',  ( -0.3420201433256627732, -0.9396926207859105373, 0.000000000000000000 ) ) ;
#9045=ADVANCED_FACE ( 'NONE', ( #4541 ), #10186, .F. ) ;
#9063=VECTOR ( 'NONE', #5864, 1000.000000000000000 ) ;
#9068=CARTESIAN_POINT ( 'NONE',  ( 0.000000000000000000, -4.000000000000000000, -12.00000000000000000 ) ) ;
#9072=ORIENTED_EDGE ( 'NONE', *, *, #2618, .T. ) ;
#9073=PLANE ( 'NONE',  #6411 ) ;
#9077=LINE ( 'NONE', #1917, #6614 ) ;
#9080=AXIS2_PLACEMENT_3D ( 'NONE', #9342, #2077, #3709 ) ;
#9082=VECTOR ( 'NONE', #9460, 1000.000000000000000 ) ;
#9084=CARTESIAN_POINT ( 'NONE',  ( 0.000000000000000000, -10.00000000000000000, -12.00000000000000000 ) ) ;
#9086=DIRECTION ( 'NONE',  ( 0.000000000000000000, -1.000000000000000000, 0.000000000000000000 ) ) ;
#9097=LINE ( 'NONE', #5846, #1852 ) ;
#9098=CARTESIAN_POINT ( 'NONE',  ( 23.25451694676619496, 6.000000000000000000, 0.000000000000000000 ) ) ;
#9106=CARTESIAN_POINT ( 'NONE',  ( 24.68830583033274806, 3.750000000000000000, -12.00000000000000000 ) ) ;
#9112=ORIENTED_EDGE ( 'NONE', *, *, #3902, .T. ) ;
#9116=CARTESIAN_POINT ( 'NONE',  ( 25.00000000000000000, -7.750000000000000000, 0.000000000000000000 ) ) ;
#9117=CARTESIAN_POINT ( 'NONE',  ( 1.868979409283444415, -10.02539999999999942, -12.00000000000000000 ) ) ;
#9131=VECTOR ( 'NONE', #666, 1000.000000000000000 ) ;
#9136=CARTESIAN_POINT ( 'NONE',  ( 8.152164709283445276, 6.025400000000000311, -12.00000000000000000 ) ) ;
#9142=EDGE_LOOP ( 'NONE', ( #2987, #5464, #1219, #3209 ) ) ;
#9143=VECTOR ( 'NONE', #2115, 1000.000000000000000 ) ;
#9150=DIRECTION ( 'NONE',  ( -0.000000000000000000, -0.000000000000000000, 1.000000000000000000 ) ) ;
#9154=ORIENTED_EDGE ( 'NONE', *, *, #7841, .T. ) ;
#9156=VECTOR ( 'NONE', #10373, 1000.000000000000000 ) ;
#9158=CARTESIAN_POINT ( 'NONE',  ( 22.43558391966725907, -7.750000000000000000, -12.00000000000000000 ) ) ;
#9163=VECTOR ( 'NONE', #10317, 1000.000000000000000 ) ;
#9165=ORIENTED_EDGE ( 'NONE', *, *, #1500, .T. ) ;
#9166=EDGE_CURVE ( 'NONE', #7999, #1996, #5239, .T. ) ;
#9169=AXIS2_PLACEMENT_3D ( 'NONE', #1411, #4636, #5227 ) ;
#9172=DIRECTION ( 'NONE',  ( -1.000000000000000000, -0.000000000000000000, -0.000000000000000000 ) ) ;
#9174=ORIENTED_EDGE ( 'NONE', *, *, #2628, .F. ) ;
#9178=VERTEX_POINT ( 'NONE', #8534 ) ;
#9179=ADVANCED_FACE ( 'NONE', ( #10235 ), #5391, .F. ) ;
#9180=DIRECTION ( 'NONE',  ( 0.3420201433256627732, 0.9396926207859105373, 0.000000000000000000 ) ) ;
#9181=CARTESIAN_POINT ( 'NONE',  ( 0.000000000000000000, -7.750000000000000000, 0.000000000000000000 ) ) ;
#9190=EDGE_CURVE ( 'NONE', #7022, #1643, #1421, .T. ) ;
#9195=EDGE_CURVE ( 'NONE', #4800, #4582, #1534, .T. ) ;
#9200=LINE ( 'NONE', #7764, #6083 ) ;
#9203=VERTEX_POINT ( 'NONE', #9545 ) ;
#9205=ORIENTED_EDGE ( 'NONE', *, *, #6286, .T. ) ;
#9207=DIRECTION ( 'NONE',  ( -0.000000000000000000, 1.000000000000000000, 0.000000000000000000 ) ) ;
#9209=ORIENTED_EDGE ( 'NONE', *, *, #4450, .F. ) ;
#9213=VERTEX_POINT ( 'NONE', #7944 ) ;
#9217=EDGE_CURVE ( 'NONE', #1592, #1146, #10399, .T. ) ;
#9222=ORIENTED_EDGE ( 'NONE', *, *, #5582, .F. ) ;
#9229=LINE ( 'NONE', #5087, #10356 ) ;
#9230=EDGE_CURVE ( 'NONE', #7067, #5890, #3279, .T. ) ;
#9231=FACE_OUTER_BOUND ( 'NONE', #5905, .T. ) ;
#9236=VECTOR ( 'NONE', #1895, 1000.000000000000000 ) ;
#9242=AXIS2_PLACEMENT_3D ( 'NONE', #5094, #1869, #5145 ) ;
#9248=LINE ( 'NONE', #5524, #9082 ) ;
#9260=CARTESIAN_POINT ( 'NONE',  ( 1.868979409283444415, 6.025400000000000311, -12.00000000000000000 ) ) ;
#9271=DIRECTION ( 'NONE',  ( -0.000000000000000000, 1.000000000000000000, 0.000000000000000000 ) ) ;
#9284=CARTESIAN_POINT ( 'NONE',  ( 19.29399126966725575, 3.750000000000000000, -12.00000000000000000 ) ) ;
#9286=CARTESIAN_POINT ( 'NONE',  ( 15.52899435786730997, -15.65209171435138735, 0.000000000000000000 ) ) ;
#9290=ADVANCED_FACE ( 'NONE', ( #2489 ), #5701, .F. ) ;
#9294=LINE ( 'NONE', #10305, #10014 ) ;
#9295=VECTOR ( 'NONE', #2809, 1000.000000000000000 ) ;
#9301=PLANE ( 'NONE',  #1530 ) ;
#9302=VECTOR ( 'NONE', #2196, 1000.000000000000000 ) ;
#9317=ORIENTED_EDGE ( 'NONE', *, *, #1658, .T. ) ;
#9320=ADVANCED_FACE ( 'NONE', ( #1691 ), #8165, .T. ) ;
#9321=FILL_AREA_STYLE_COLOUR ( '', #8890 ) ;
#9324=VECTOR ( 'NONE', #119, 1000.000000000000000 ) ;
#9326=CARTESIAN_POINT ( 'NONE',  ( 10.69739119071655686, -10.02539999999999942, -12.00000000000000000 ) ) ;
#9328=VERTEX_POINT ( 'NONE', #4698 ) ;
#9330=AXIS2_PLACEMENT_3D ( 'NONE', #6157, #4306, #2830 ) ;
#9338=CARTESIAN_POINT ( 'NONE',  ( 10.68814634676619590, 6.000000000000000000, 0.000000000000000000 ) ) ;
#9342=CARTESIAN_POINT ( 'NONE',  ( 13.01080596966725622, -7.750000000000000000, -12.00000000000000000 ) ) ;
#9344=FACE_OUTER_BOUND ( 'NONE', #9638, .T. ) ;
#9351=DIRECTION ( 'NONE',  ( -1.000000000000000000, 0.000000000000000000, -0.000000000000000000 ) ) ;
#9352=EDGE_CURVE ( 'NONE', #2796, #7411, #791, .T. ) ;
#9355=EDGE_CURVE ( 'NONE', #3874, #4442, #7250, .T. ) ;
#9357=ORIENTED_EDGE ( 'NONE', *, *, #4736, .F. ) ;
#9377=AXIS2_PLACEMENT_3D ( 'NONE', #5347, #1481, #6293 ) ;
#9378=ORIENTED_EDGE ( 'NONE', *, *, #3054, .T. ) ;
#9379=CARTESIAN_POINT ( 'NONE',  ( 0.000000000000000000, 6.000000000000000000, -12.00000000000000000 ) ) ;
#9380=DIRECTION ( 'NONE',  ( 0.000000000000000000, 0.000000000000000000, -1.000000000000000000 ) ) ;
#9385=ORIENTED_EDGE ( 'NONE', *, *, #8389, .T. ) ;
#9391=CARTESIAN_POINT ( 'NONE',  ( 20.12216914071655793, 6.025400000000000311, -12.00000000000000000 ) ) ;
#9393=CARTESIAN_POINT ( 'NONE',  ( 1.878224253233805818, 6.000000000000000000, 0.000000000000000000 ) ) ;
#9394=PLANE ( 'NONE',  #3823 ) ;
#9399=AXIS2_PLACEMENT_3D ( 'NONE', #7541, #9086, #1820 ) ;
#9404=VERTEX_POINT ( 'NONE', #9338 ) ;
#9408=CARTESIAN_POINT ( 'NONE',  ( 1.263368396766194612, -10.00000000000000000, 0.000000000000000000 ) ) ;
#9411=AXIS2_PLACEMENT_3D ( 'NONE', #10180, #419, #7683 ) ;
#9413=LINE ( 'NONE', #2147, #1190 ) ;
#9417=ADVANCED_FACE ( 'NONE', ( #9231 ), #1067, .F. ) ;
#9419=EDGE_CURVE ( 'NONE', #4407, #4215, #3703, .T. ) ;
#9422=ORIENTED_EDGE ( 'NONE', *, *, #1778, .F. ) ;
#9428=CARTESIAN_POINT ( 'NONE',  ( 0.000000000000000000, 3.750000000000000000, 0.000000000000000000 ) ) ;
#9431=CARTESIAN_POINT ( 'NONE',  ( 15.52899435786730997, 11.65209171435138735, 0.000000000000000000 ) ) ;
#9432=EDGE_CURVE ( 'NONE', #6552, #3824, #7534, .T. ) ;
#9437=CARTESIAN_POINT ( 'NONE',  ( 25.57717656966725883, -7.750000000000000000, -12.00000000000000000 ) ) ;
#9438=EDGE_LOOP ( 'NONE', ( #8800, #4180, #6774, #5635 ) ) ;
#9443=CARTESIAN_POINT ( 'NONE',  ( 15.26352788033274699, 3.750000000000000000, -12.00000000000000000 ) ) ;
#9444=CARTESIAN_POINT ( 'NONE',  ( 9.869213319667256457, 3.750000000000000000, -12.00000000000000000 ) ) ;
#9450=DIRECTION ( 'NONE',  ( 0.000000000000000000, 0.000000000000000000, -1.000000000000000000 ) ) ;
#9451=PLANE ( 'NONE',  #2182 ) ;
#9456=DIRECTION ( 'NONE',  ( 0.000000000000000000, 1.000000000000000000, 0.000000000000000000 ) ) ;
#9460=DIRECTION ( 'NONE',  ( 0.000000000000000000, 0.000000000000000000, 1.000000000000000000 ) ) ;
#9463=EDGE_CURVE ( 'NONE', #10205, #10233, #1273, .T. ) ;
#9480=DIRECTION ( 'NONE',  ( 0.3420201433256627732, -0.9396926207859105373, 0.000000000000000000 ) ) ;
#9485=ORIENTED_EDGE ( 'NONE', *, *, #8887, .F. ) ;
#9489=EDGE_LOOP ( 'NONE', ( #7767, #3041, #5325, #4473 ) ) ;
#9490=EDGE_CURVE ( 'NONE', #4979, #931, #7040, .T. ) ;
#9497=VECTOR ( 'NONE', #7170, 1000.000000000000000 ) ;
#9510=VECTOR ( 'NONE', #5779, 1000.000000000000000 ) ;
#9518=DIRECTION ( 'NONE',  ( -0.000000000000000000, -0.000000000000000000, 1.000000000000000000 ) ) ;
#9541=DIRECTION ( 'NONE',  ( -0.9396926207859105373, 0.3420201433256627732, 0.000000000000000000 ) ) ;
#9545=CARTESIAN_POINT ( 'NONE',  ( 13.82973899676619745, -10.00000000000000000, -12.00000000000000000 ) ) ;
#9551=EDGE_CURVE ( 'NONE', #2276, #10233, #3919, .T. ) ;
#9552=EDGE_CURVE ( 'NONE', #3797, #7067, #4702, .T. ) ;
#9559=CARTESIAN_POINT ( 'NONE',  ( 19.29399126966725575, 3.750000000000000000, -12.00000000000000000 ) ) ;
#9560=DIRECTION ( 'NONE',  ( 0.000000000000000000, 0.000000000000000000, 1.000000000000000000 ) ) ;
#9564=ADVANCED_FACE ( 'NONE', ( #10239 ), #1320, .F. ) ;
#9569=PLANE ( 'NONE',  #4158 ) ;
#9580=ORIENTED_EDGE ( 'NONE', *, *, #7138, .T. ) ;
#9592=ORIENTED_EDGE ( 'NONE', *, *, #9551, .T. ) ;
#9593=VECTOR ( 'NONE', #446, 1000.000000000000000 ) ;
#9596=DIRECTION ( 'NONE',  ( 0.000000000000000000, 0.000000000000000000, 1.000000000000000000 ) ) ;
#9599=CARTESIAN_POINT ( 'NONE',  ( 4.432609873715410487, -11.61333805414684761, 0.000000000000000000 ) ) ;
#9601=ORIENTED_EDGE ( 'NONE', *, *, #7477, .F. ) ;
#9603=ADVANCED_FACE ( 'NONE', ( #579 ), #4766, .F. ) ;
#9612=DIRECTION ( 'NONE',  ( 0.000000000000000000, 0.000000000000000000, -1.000000000000000000 ) ) ;
#9614=EDGE_CURVE ( 'NONE', #7286, #3593, #3074, .T. ) ;
#9619=LINE ( 'NONE', #10303, #3779 ) ;
#9622=PLANE ( 'NONE',  #6678 ) ;
#9624=ORIENTED_EDGE ( 'NONE', *, *, #2996, .T. ) ;
#9636=LINE ( 'NONE', #10491, #10021 ) ;
#9638=EDGE_LOOP ( 'NONE', ( #5581, #821, #1000, #5071 ) ) ;
#9640=CARTESIAN_POINT ( 'NONE',  ( 16.97133164676619899, 6.000000000000000888, -12.00000000000000000 ) ) ;
#9642=LINE ( 'NONE', #10328, #5432 ) ;
#9645=ORIENTED_EDGE ( 'NONE', *, *, #10327, .T. ) ;
#9648=VECTOR ( 'NONE', #7260, 1000.000000000000000 ) ;
#9650=VERTEX_POINT ( 'NONE', #9957 ) ;
#9657=CARTESIAN_POINT ( 'NONE',  ( 2.697157280332745266, 3.750000000000000000, 0.000000000000000000 ) ) ;
#9658=VECTOR ( 'NONE', #7786, 1000.000000000000000 ) ;
#9659=ORIENTED_EDGE ( 'NONE', *, *, #83, .T. ) ;
#9665=AXIS2_PLACEMENT_3D ( 'NONE', #6767, #1856, #1003 ) ;
#9666=CARTESIAN_POINT ( 'NONE',  ( 5.838749930332745919, 3.750000000000000000, 0.000000000000000000 ) ) ;
#9671=CARTESIAN_POINT ( 'NONE',  ( 13.83898384071655840, -10.02539999999999942, 0.000000000000000000 ) ) ;
#9673=ORIENTED_EDGE ( 'NONE', *, *, #6523, .T. ) ;
#9682=CARTESIAN_POINT ( 'NONE',  ( 5.019816903233806471, 6.000000000000000000, 0.000000000000000000 ) ) ;
#9684=DIRECTION ( 'NONE',  ( -0.9396926207859105373, 0.3420201433256627732, 0.000000000000000000 ) ) ;
#9685=VECTOR ( 'NONE', #6900, 1000.000000000000000 ) ;
#9697=ORIENTED_EDGE ( 'NONE', *, *, #5738, .T. ) ;
#9699=LINE ( 'NONE', #8047, #1016 ) ;
#9702=VERTEX_POINT ( 'NONE', #1140 ) ;
#9707=ORIENTED_EDGE ( 'NONE', *, *, #8514, .F. ) ;
#9709=DIRECTION ( 'NONE',  ( -1.000000000000000000, -0.000000000000000000, 0.000000000000000000 ) ) ;
#9713=VERTEX_POINT ( 'NONE', #6747 ) ;
#9726=PRODUCT_CONTEXT ( 'NONE', #6338, 'mechanical' ) ;
#9729=CARTESIAN_POINT ( 'NONE',  ( 0.000000000000000000, -10.00000000000000000, -12.00000000000000000 ) ) ;
#9734=DIRECTION ( 'NONE',  ( 1.000000000000000000, -0.000000000000000000, -0.000000000000000000 ) ) ;
#9736=EDGE_CURVE ( 'NONE', #8270, #4252, #3476, .T. ) ;
#9742=DIRECTION ( 'NONE',  ( 0.3420201433256627732, -0.9396926207859105373, 0.000000000000000000 ) ) ;
#9745=VECTOR ( 'NONE', #3707, 1000.000000000000000 ) ;
#9747=DIRECTION ( 'NONE',  ( -1.000000000000000000, -0.000000000000000000, 0.000000000000000000 ) ) ;
#9748=VERTEX_POINT ( 'NONE', #5113 ) ;
#9753=ORIENTED_EDGE ( 'NONE', *, *, #8044, .T. ) ;
#9755=PLANE ( 'NONE',  #3805 ) ;
#9756=CARTESIAN_POINT ( 'NONE',  ( 0.000000000000000000, 6.000000000000000000, -12.00000000000000000 ) ) ;
#9757=VERTEX_POINT ( 'NONE', #2721 ) ;
#9765=ORIENTED_EDGE ( 'NONE', *, *, #1057, .T. ) ;
#9767=VECTOR ( 'NONE', #7273, 1000.000000000000000 ) ;
#9770=CARTESIAN_POINT ( 'NONE',  ( 20.72778015323380885, -10.00000000000000000, 0.000000000000000000 ) ) ;
#9772=LINE ( 'NONE', #4772, #9648 ) ;
#9778=CARTESIAN_POINT ( 'NONE',  ( 0.000000000000000000, 6.000000000000000000, 0.000000000000000000 ) ) ;
#9779=CARTESIAN_POINT ( 'NONE',  ( 0.000000000000000000, -4.000000000000000000, -12.00000000000000000 ) ) ;
#9780=PLANE ( 'NONE',  #2978 ) ;
#9782=CARTESIAN_POINT ( 'NONE',  ( 20.71853530928344611, -10.02539999999999942, -12.00000000000000000 ) ) ;
#9786=EDGE_CURVE ( 'NONE', #3241, #247, #4201, .T. ) ;
#9788=ORIENTED_EDGE ( 'NONE', *, *, #10446, .F. ) ;
#9792=DIRECTION ( 'NONE',  ( 0.3420201433256627732, -0.9396926207859105373, 0.000000000000000000 ) ) ;
#9793=ORIENTED_EDGE ( 'NONE', *, *, #9914, .F. ) ;
#9795=CARTESIAN_POINT ( 'NONE',  ( 19.29399126966725575, 3.750000000000000000, -12.00000000000000000 ) ) ;
#9800=ORIENTED_EDGE ( 'NONE', *, *, #4097, .T. ) ;
#9810=EDGE_LOOP ( 'NONE', ( #5684, #3955, #9788, #7349 ) ) ;
#9815=CARTESIAN_POINT ( 'NONE',  ( 0.000000000000000000, -10.00000000000000000, 0.000000000000000000 ) ) ;
#9818=FACE_OUTER_BOUND ( 'NONE', #3075, .T. ) ;
#9826=LINE ( 'NONE', #2558, #747 ) ;
#9831=VECTOR ( 'NONE', #2601, 1000.000000000000000 ) ;
#9845=ORIENTED_EDGE ( 'NONE', *, *, #4946, .F. ) ;
#9849=EDGE_CURVE ( 'NONE', #3187, #5332, #2516, .T. ) ;
#9852=VECTOR ( 'NONE', #526, 1000.000000000000000 ) ;
#9859=ORIENTED_EDGE ( 'NONE', *, *, #8455, .T. ) ;
#9869=ORIENTED_EDGE ( 'NONE', *, *, #7115, .T. ) ;
#9870=CARTESIAN_POINT ( 'NONE',  ( 0.000000000000000000, 6.000000000000000000, -12.00000000000000000 ) ) ;
#9871=DIRECTION ( 'NONE',  ( 0.3420201433256627732, -0.9396926207859105373, 0.000000000000000000 ) ) ;
#9872=CARTESIAN_POINT ( 'NONE',  ( 7.555798540716556211, -10.02539999999999942, -12.00000000000000000 ) ) ;
#9884=AXIS2_PLACEMENT_3D ( 'NONE', #8685, #8484, #1370 ) ;
#9885=CARTESIAN_POINT ( 'NONE',  ( 0.000000000000000000, 0.000000000000000000, -10.00000000000000000 ) ) ;
#9887=PLANE ( 'NONE',  #9399 ) ;
#9890=ADVANCED_FACE ( 'NONE', ( #7704 ), #441, .F. ) ;
#9893=DIRECTION ( 'NONE',  ( 0.3420201433256627732, -0.9396926207859105373, 0.000000000000000000 ) ) ;
#9894=ORIENTED_EDGE ( 'NONE', *, *, #3079, .T. ) ;
#9905=EDGE_LOOP ( 'NONE', ( #147, #3882, #463, #549, #4681, #857, #6121, #5685, #1406, #6539, #589, #6706, #6591, #600, #8481, #6859, #10469, #4578, #490, #10493, #6483, #7625, #443, #3975, #2485, #8217, #7358, #3360, #9753, #10261, #3596, #10304, #8532, #9800, #10309, #6150 ) ) ;
#9907=VECTOR ( 'NONE', #6982, 1000.000000000000000 ) ;
#9911=ORIENTED_EDGE ( 'NONE', *, *, #4178, .T. ) ;
#9914=EDGE_CURVE ( 'NONE', #5526, #928, #10149, .T. ) ;
#9920=ORIENTED_EDGE ( 'NONE', *, *, #8493, .T. ) ;
#9922=PLANE ( 'NONE',  #1205 ) ;
#9923=LINE ( 'NONE', #2752, #4902 ) ;
#9926=VECTOR ( 'NONE', #99, 1000.000000000000000 ) ;
#9927=ADVANCED_FACE ( 'NONE', ( #4613 ), #4779, .T. ) ;
#9937=CARTESIAN_POINT ( 'NONE',  ( 16.98057649071655817, -10.02539999999999942, 0.000000000000000000 ) ) ;
#9938=EDGE_CURVE ( 'NONE', #2255, #2670, #9619, .T. ) ;
#9946=ORIENTED_EDGE ( 'NONE', *, *, #4254, .T. ) ;
#9949=CARTESIAN_POINT ( 'NONE',  ( 7.555798540716556211, -10.02539999999999942, -12.00000000000000000 ) ) ;
#9951=VERTEX_POINT ( 'NONE', #2984 ) ;
#9955=EDGE_CURVE ( 'NONE', #10377, #4895, #7104, .T. ) ;
#9957=CARTESIAN_POINT ( 'NONE',  ( 15.26352788033274699, -7.750000000000000000, 0.000000000000000000 ) ) ;
#9960=ORIENTED_EDGE ( 'NONE', *, *, #8079, .T. ) ;
#9970=EDGE_CURVE ( 'NONE', #1402, #946, #6413, .T. ) ;
#9971=ORIENTED_EDGE ( 'NONE', *, *, #7678, .F. ) ;
#9972=DIRECTION ( 'NONE',  ( 0.3420201433256627732, 0.9396926207859105373, -0.000000000000000000 ) ) ;
#9977=ADVANCED_FACE ( 'NONE', ( #7268 ), #5566, .F. ) ;
#9988=VECTOR ( 'NONE', #722, 1000.000000000000000 ) ;
#9991=VECTOR ( 'NONE', #10339, 1000.000000000000000 ) ;
#9995=AXIS2_PLACEMENT_3D ( 'NONE', #957, #9014, #5031 ) ;
#10000=CARTESIAN_POINT ( 'NONE',  ( 0.000000000000000000, 0.000000000000000000, -2.000000000000000000 ) ) ;
#10003=VECTOR ( 'NONE', #4368, 1000.000000000000000 ) ;
#10006=ADVANCED_FACE ( 'NONE', ( #2293 ), #5517, .T. ) ;
#10008=EDGE_CURVE ( 'NONE', #5295, #2931, #703, .T. ) ;
#10012=ORIENTED_EDGE ( 'NONE', *, *, #7664, .F. ) ;
#10013=LINE ( 'NONE', #6909, #3313 ) ;
#10014=VECTOR ( 'NONE', #8503, 1000.000000000000000 ) ;
#10021=VECTOR ( 'NONE', #2256, 1000.000000000000000 ) ;
#10028=VERTEX_POINT ( 'NONE', #170 ) ;
#10032=ORIENTED_EDGE ( 'NONE', *, *, #9230, .T. ) ;
#10034=DIRECTION ( 'NONE',  ( 0.9396926207859105373, -0.3420201433256627732, 0.000000000000000000 ) ) ;
#10037=ORIENTED_EDGE ( 'NONE', *, *, #6848, .F. ) ;
#10038=CARTESIAN_POINT ( 'NONE',  ( 11.29375735928344504, -10.02539999999999942, -12.00000000000000000 ) ) ;
#10044=CARTESIAN_POINT ( 'NONE',  ( 5.838749930332745919, -7.750000000000000000, -12.00000000000000000 ) ) ;
#10053=FACE_OUTER_BOUND ( 'NONE', #6018, .T. ) ;
#10061=EDGE_LOOP ( 'NONE', ( #10123, #8885, #7998, #4850 ) ) ;
#10062=EDGE_LOOP ( 'NONE', ( #6545, #4257, #5165, #2434 ) ) ;
#10063=CARTESIAN_POINT ( 'NONE',  ( 0.000000000000000000, 6.000000000000000000, -12.00000000000000000 ) ) ;
#10065=EDGE_LOOP ( 'NONE', ( #4114, #1419, #8019, #9673 ) ) ;
#10072=CARTESIAN_POINT ( 'NONE',  ( 17.57694265928344635, 6.025400000000000311, -12.00000000000000000 ) ) ;
#10074=ORIENTED_EDGE ( 'NONE', *, *, #2996, .F. ) ;
#10092=LINE ( 'NONE', #7905, #2807 ) ;
#10101=EDGE_LOOP ( 'NONE', ( #1892, #6272, #3783, #5324 ) ) ;
#10102=DIRECTION ( 'NONE',  ( -1.000000000000000000, 0.000000000000000000, -0.000000000000000000 ) ) ;
#10104=PLANE ( 'NONE',  #9330 ) ;
#10114=ADVANCED_FACE ( 'NONE', ( #8341 ), #6520, .F. ) ;
#10115=EDGE_LOOP ( 'NONE', ( #3832, #10439, #4635, #2429 ) ) ;
#10116=DIRECTION ( 'NONE',  ( 0.000000000000000000, 0.000000000000000000, -1.000000000000000000 ) ) ;
#10119=EDGE_LOOP ( 'NONE', ( #6561, #1653, #7741, #6188 ) ) ;
#10123=ORIENTED_EDGE ( 'NONE', *, *, #8044, .F. ) ;
#10124=CARTESIAN_POINT ( 'NONE',  ( 19.29399126966725575, 3.750000000000000000, 0.000000000000000000 ) ) ;
#10128=VERTEX_POINT ( 'NONE', #8128 ) ;
#10130=LINE ( 'NONE', #9326, #8623 ) ;
#10141=CARTESIAN_POINT ( 'NONE',  ( 9.869213319667256457, 3.750000000000000000, -12.00000000000000000 ) ) ;
#10142=DIRECTION ( 'NONE',  ( 0.000000000000000000, 0.000000000000000000, 1.000000000000000000 ) ) ;
#10149=LINE ( 'NONE', #4831, #7337 ) ;
#10153=LINE ( 'NONE', #4564, #6270 ) ;
#10160=VECTOR ( 'NONE', #3650, 1000.000000000000000 ) ;
#10163=VERTEX_POINT ( 'NONE', #5670 ) ;
#10168=AXIS2_PLACEMENT_3D ( 'NONE', #2106, #5331, #7830 ) ;
#10173=DIRECTION ( 'NONE',  ( -0.3420201433256627732, 0.9396926207859105373, 0.000000000000000000 ) ) ;
#10179=VECTOR ( 'NONE', #1066, 1000.000000000000000 ) ;
#10180=CARTESIAN_POINT ( 'NONE',  ( 0.000000000000000000, -10.00000000000000000, -12.00000000000000000 ) ) ;
#10181=DIRECTION ( 'NONE',  ( 0.3420201433256627732, -0.9396926207859105373, 0.000000000000000000 ) ) ;
#10185=VECTOR ( 'NONE', #6528, 1000.000000000000000 ) ;
#10186=PLANE ( 'NONE',  #4815 ) ;
#10191=VECTOR ( 'NONE', #3754, 1000.000000000000000 ) ;
#10192=VECTOR ( 'NONE', #5268, 1000.000000000000000 ) ;
#10196=DIRECTION ( 'NONE',  ( -0.000000000000000000, -0.000000000000000000, 1.000000000000000000 ) ) ;
#10197=PLANE ( 'NONE',  #6697 ) ;
#10205=VERTEX_POINT ( 'NONE', #6573 ) ;
#10206=LINE ( 'NONE', #8601, #2884 ) ;
#10207=DIRECTION ( 'NONE',  ( 0.3420201433256627732, 0.9396926207859105373, 0.000000000000000000 ) ) ;
#10209=CARTESIAN_POINT ( 'NONE',  ( 8.161409553233806236, -10.00000000000000000, 0.000000000000000000 ) ) ;
#10211=EDGE_CURVE ( 'NONE', #4442, #2276, #9826, .T. ) ;
#10212=DIRECTION ( 'NONE',  ( 1.000000000000000000, 0.000000000000000000, 0.000000000000000000 ) ) ;
#10213=LINE ( 'NONE', #7821, #3228 ) ;
#10225=CARTESIAN_POINT ( 'NONE',  ( 20.72778015323380529, -10.00000000000000000, -12.00000000000000000 ) ) ;
#10232=EDGE_CURVE ( 'NONE', #3542, #8622, #4989, .T. ) ;
#10233=VERTEX_POINT ( 'NONE', #7425 ) ;
#10235=FACE_OUTER_BOUND ( 'NONE', #1678, .T. ) ;
#10237=ORIENTED_EDGE ( 'NONE', *, *, #985, .T. ) ;
#10239=FACE_OUTER_BOUND ( 'NONE', #7671, .T. ) ;
#10240=CARTESIAN_POINT ( 'NONE',  ( 25.00000000000000000, 3.750000000000000000, 0.000000000000000000 ) ) ;
#10243=DIRECTION ( 'NONE',  ( -0.000000000000000000, 1.000000000000000000, -0.000000000000000000 ) ) ;
#10252=VECTOR ( 'NONE', #8026, 1000.000000000000000 ) ;
#10254=EDGE_CURVE ( 'NONE', #7411, #2729, #7582, .T. ) ;
#10257=EDGE_LOOP ( 'NONE', ( #1727, #6654, #3645, #2084 ) ) ;
#10261=ORIENTED_EDGE ( 'NONE', *, *, #8272, .T. ) ;
#10262=AXIS2_PLACEMENT_3D ( 'NONE', #8104, #3429, #944 ) ;
#10269=VECTOR ( 'NONE', #10142, 1000.000000000000000 ) ;
#10272=CARTESIAN_POINT ( 'NONE',  ( -0.000000000000000000, -4.000000000000000000, -2.000000000000000000 ) ) ;
#10276=CARTESIAN_POINT ( 'NONE',  ( 12.12193523033274545, -7.750000000000000000, -12.00000000000000000 ) ) ;
#10282=FACE_OUTER_BOUND ( 'NONE', #7255, .T. ) ;
#10291=CARTESIAN_POINT ( 'NONE',  ( 10.68814634676619413, 6.000000000000000000, -12.00000000000000000 ) ) ;
#10298=LINE ( 'NONE', #3711, #3702 ) ;
#10301=EDGE_CURVE ( 'NONE', #5749, #717, #7641, .T. ) ;
#10303=CARTESIAN_POINT ( 'NONE',  ( 4.404961046766194599, 6.000000000000000000, -12.00000000000000000 ) ) ;
#10304=ORIENTED_EDGE ( 'NONE', *, *, #3333, .F. ) ;
#10305=CARTESIAN_POINT ( 'NONE',  ( 0.000000000000000000, -10.00000000000000000, -12.00000000000000000 ) ) ;
#10309=ORIENTED_EDGE ( 'NONE', *, *, #9166, .F. ) ;
#10315=VERTEX_POINT ( 'NONE', #7535 ) ;
#10316=ORIENTED_EDGE ( 'NONE', *, *, #8493, .F. ) ;
#10317=DIRECTION ( 'NONE',  ( 0.000000000000000000, 0.000000000000000000, 1.000000000000000000 ) ) ;
#10327=EDGE_CURVE ( 'NONE', #4315, #3824, #6832, .T. ) ;
#10328=CARTESIAN_POINT ( 'NONE',  ( 23.25451694676619496, -10.00000000000000000, -12.00000000000000000 ) ) ;
#10330=AXIS2_PLACEMENT_3D ( 'NONE', #9782, #9684, #3302 ) ;
#10335=CARTESIAN_POINT ( 'NONE',  ( 5.838749930332745919, 3.750000000000000000, -12.00000000000000000 ) ) ;
#10339=DIRECTION ( 'NONE',  ( -1.000000000000000000, -0.000000000000000000, -0.000000000000000000 ) ) ;
#10356=VECTOR ( 'NONE', #2705, 1000.000000000000000 ) ;
#10369=DIRECTION ( 'NONE',  ( 0.000000000000000000, 0.000000000000000000, -1.000000000000000000 ) ) ;
#10372=LINE ( 'NONE', #3833, #7948 ) ;
#10373=DIRECTION ( 'NONE',  ( 0.000000000000000000, 0.000000000000000000, 1.000000000000000000 ) ) ;
#10377=VERTEX_POINT ( 'NONE', #5299 ) ;
#10381=CARTESIAN_POINT ( 'NONE',  ( 20.12216914071655793, -10.02539999999999942, 0.000000000000000000 ) ) ;
#10384=DIRECTION ( 'NONE',  ( 0.3420201433256627732, -0.9396926207859105373, 0.000000000000000000 ) ) ;
#10387=DIRECTION ( 'NONE',  ( 0.000000000000000000, 0.000000000000000000, 1.000000000000000000 ) ) ;
#10394=PLANE ( 'NONE',  #5836 ) ;
#10399=LINE ( 'NONE', #1951, #4793 ) ;
#10403=AXIS2_PLACEMENT_3D ( 'NONE', #4560, #3667, #8552 ) ;
#10405=ORIENTED_EDGE ( 'NONE', *, *, #7678, .T. ) ;
#10406=EDGE_CURVE ( 'NONE', #5555, #1004, #8639, .T. ) ;
#10410=LINE ( 'NONE', #4658, #115 ) ;
#10411=CARTESIAN_POINT ( 'NONE',  ( 15.26352788033274699, 3.750000000000000000, 0.000000000000000000 ) ) ;
#10422=LINE ( 'NONE', #2192, #604 ) ;
#10424=DIRECTION ( 'NONE',  ( 0.3420201433256627732, 0.9396926207859105373, -0.000000000000000000 ) ) ;
#10425=VECTOR ( 'NONE', #3610, 1000.000000000000000 ) ;
#10427=CARTESIAN_POINT ( 'NONE',  ( 20.72778015323380885, 6.000000000000000000, -12.00000000000000000 ) ) ;
#10432=ORIENTED_EDGE ( 'NONE', *, *, #4198, .T. ) ;
#10433=EDGE_CURVE ( 'NONE', #5848, #6919, #7145, .T. ) ;
#10435=CARTESIAN_POINT ( 'NONE',  ( 17.58618750323380553, 6.000000000000000000, -12.00000000000000000 ) ) ;
#10437=LINE ( 'NONE', #2206, #1537 ) ;
#10439=ORIENTED_EDGE ( 'NONE', *, *, #784, .F. ) ;
#10445=VECTOR ( 'NONE', #707, 1000.000000000000000 ) ;
#10446=EDGE_CURVE ( 'NONE', #9404, #4215, #2972, .T. ) ;
#10450=DIRECTION ( 'NONE',  ( 0.3420201433256627732, -0.9396926207859105373, 0.000000000000000000 ) ) ;
#10452=ORIENTED_EDGE ( 'NONE', *, *, #4810, .T. ) ;
#10463=DIRECTION ( 'NONE',  ( 0.9396926207859105373, -0.3420201433256627732, 0.000000000000000000 ) ) ;
#10466=CARTESIAN_POINT ( 'NONE',  ( 6.727620669667255804, 3.750000000000000000, -12.00000000000000000 ) ) ;
#10469=ORIENTED_EDGE ( 'NONE', *, *, #1624, .T. ) ;
#10480=PLANE ( 'NONE',  #3316 ) ;
#10483=CARTESIAN_POINT ( 'NONE',  ( 0.000000000000000000, 6.000000000000000000, 0.000000000000000000 ) ) ;
#10489=ORIENTED_EDGE ( 'NONE', *, *, #1635, .T. ) ;
#10490=VERTEX_POINT ( 'NONE', #10240 ) ;
#10491=CARTESIAN_POINT ( 'NONE',  ( 17.57694265928344635, -10.02539999999999942, -12.00000000000000000 ) ) ;
#10492=DIRECTION ( 'NONE',  ( -0.3420201433256627732, -0.9396926207859105373, 0.000000000000000000 ) ) ;
#10493=ORIENTED_EDGE ( 'NONE', *, *, #63, .F. ) ;
ENDSEC;
END-ISO-10303-21;
